ISO-10303-21;
HEADER;
FILE_DESCRIPTION (('STEP AP214'),
    '1' );
FILE_NAME ('Locking Springs.step',
    '2026-10-06T10:59:17',
    ( '' ),
    ( '' ),
    'SwSTEP 2.0',
    'SolidWorks 2026',
    '' );
FILE_SCHEMA (( 'AUTOMOTIVE_DESIGN' ));
ENDSEC;

DATA;
#8=EDGE_CURVE ( 'NONE', #10795, #13483, #5393, .T. ) ;
#23=FACE_OUTER_BOUND ( 'NONE', #2715, .T. ) ;
#29=DIRECTION ( 'NONE',  ( -1.402518428993831183E-16, 1.000000000000000000, -3.469446951953617640E-16 ) ) ;
#41=ORIENTED_EDGE ( 'NONE', *, *, #20258, .F. ) ;
#43=DIRECTION ( 'NONE',  ( -1.402518428993830937E-16, 1.000000000000000000, -3.469446951953617147E-16 ) ) ;
#55=CARTESIAN_POINT ( 'NONE',  ( 27.03948732994508219, 45.16218137147969003, 73.00433879953099847 ) ) ;
#76=ADVANCED_FACE ( 'NONE', ( #16800 ), #11914, .T. ) ;
#82=ORIENTED_EDGE ( 'NONE', *, *, #15786, .F. ) ;
#95=ADVANCED_FACE ( 'NONE', ( #11803 ), #8817, .F. ) ;
#135=DIRECTION ( 'NONE',  ( 1.000000000000000000, 0.000000000000000000, 0.000000000000000000 ) ) ;
#143=ORIENTED_EDGE ( 'NONE', *, *, #10138, .T. ) ;
#151=ADVANCED_FACE ( 'NONE', ( #2321 ), #726, .T. ) ;
#215=ORIENTED_EDGE ( 'NONE', *, *, #16170, .F. ) ;
#218=DIRECTION ( 'NONE',  ( 0.000000000000000000, 0.000000000000000000, 1.000000000000000000 ) ) ;
#224=CARTESIAN_POINT ( 'NONE',  ( 31.03948732994507864, 43.16218137147969003, 76.90433879953100416 ) ) ;
#241=LINE ( 'NONE', #6730, #1600 ) ;
#242=LINE ( 'NONE', #11753, #2979 ) ;
#251=DIRECTION ( 'NONE',  ( 1.000000000000000000, 0.000000000000000000, 0.000000000000000000 ) ) ;
#272=CARTESIAN_POINT ( 'NONE',  ( 27.63948732994508717, 36.35905713404685002, 74.70433879953098710 ) ) ;
#328=AXIS2_PLACEMENT_3D ( 'NONE', #19020, #17738, #3059 ) ;
#330=DIRECTION ( 'NONE',  ( -1.402518428993831676E-16, 1.000000000000000000, -0.000000000000000000 ) ) ;
#393=VECTOR ( 'NONE', #11426, 1000.000000000000000 ) ;
#394=CARTESIAN_POINT ( 'NONE',  ( 26.43948732994507367, 45.16218137147968292, 74.70433879953098710 ) ) ;
#427=VECTOR ( 'NONE', #13805, 1000.000000000000000 ) ;
#435=APPLICATION_CONTEXT ( 'automotive_design' ) ;
#464=VECTOR ( 'NONE', #17169, 1000.000000000000114 ) ;
#483=ORIENTED_EDGE ( 'NONE', *, *, #9901, .T. ) ;
#504=FACE_OUTER_BOUND ( 'NONE', #17510, .T. ) ;
#515=ORIENTED_EDGE ( 'NONE', *, *, #17085, .T. ) ;
#516=CARTESIAN_POINT ( 'NONE',  ( 27.03948732994508930, 43.16218137147969003, 76.90433879953101837 ) ) ;
#520=EDGE_CURVE ( 'NONE', #7726, #2743, #10893, .T. ) ;
#548=ORIENTED_EDGE ( 'NONE', *, *, #4583, .T. ) ;
#611=CARTESIAN_POINT ( 'NONE',  ( 27.03948732994508930, 36.35905713404685713, 76.90433879953101837 ) ) ;
#633=ORIENTED_EDGE ( 'NONE', *, *, #11977, .T. ) ;
#674=AXIS2_PLACEMENT_3D ( 'NONE', #3348, #6948, #15057 ) ;
#715=ORIENTED_EDGE ( 'NONE', *, *, #7235, .T. ) ;
#726=CYLINDRICAL_SURFACE ( 'NONE', #8156, 1.399999999999998579 ) ;
#752=DIRECTION ( 'NONE',  ( -0.000000000000000000, -3.469446951953617147E-16, -1.000000000000000000 ) ) ;
#768=EDGE_CURVE ( 'NONE', #4756, #9174, #10932, .T. ) ;
#770=ADVANCED_FACE ( 'NONE', ( #9332 ), #13036, .T. ) ;
#779=ORIENTED_EDGE ( 'NONE', *, *, #2877, .T. ) ;
#798=CARTESIAN_POINT ( 'NONE',  ( 29.03948732994507864, 43.16218137147969003, 74.70433879953100131 ) ) ;
#892=CARTESIAN_POINT ( 'NONE',  ( 27.03948732994508930, 36.35905713404685713, 76.90433879953101837 ) ) ;
#901=EDGE_CURVE ( 'NONE', #14294, #3149, #17917, .T. ) ;
#908=CARTESIAN_POINT ( 'NONE',  ( 29.63948732994508006, 43.16218137147969003, 74.70433879953100131 ) ) ;
#933=CARTESIAN_POINT ( 'NONE',  ( 30.43948732994507722, 36.35905713404685002, 74.70433879953098710 ) ) ;
#1027=AXIS2_PLACEMENT_3D ( 'NONE', #7124, #3723, #1925 ) ;
#1028=AXIS2_PLACEMENT_3D ( 'NONE', #892, #20351, #15583 ) ;
#1030=ORIENTED_EDGE ( 'NONE', *, *, #20668, .F. ) ;
#1040=EDGE_LOOP ( 'NONE', ( #1291, #9949, #2043, #17962 ) ) ;
#1061=DIRECTION ( 'NONE',  ( 6.308085367188358095E-15, 0.000000000000000000, 1.000000000000000000 ) ) ;
#1080=EDGE_CURVE ( 'NONE', #16996, #20468, #7005, .T. ) ;
#1088=LINE ( 'NONE', #4570, #18017 ) ;
#1113=PLANE ( 'NONE',  #5087 ) ;
#1138=ORIENTED_EDGE ( 'NONE', *, *, #17818, .F. ) ;
#1145=VERTEX_POINT ( 'NONE', #9758 ) ;
#1169=CARTESIAN_POINT ( 'NONE',  ( 27.03948732994508930, 36.35905713404685713, 76.90433879953101837 ) ) ;
#1213=EDGE_CURVE ( 'NONE', #11255, #20468, #7735, .T. ) ;
#1232=ORIENTED_EDGE ( 'NONE', *, *, #4583, .F. ) ;
#1255=( LENGTH_UNIT ( ) NAMED_UNIT ( * ) SI_UNIT ( .MILLI., .METRE. ) );
#1291=ORIENTED_EDGE ( 'NONE', *, *, #9499, .F. ) ;
#1374=DIRECTION ( 'NONE',  ( -1.000000000000000000, -1.402518428993809243E-16, 6.308085367188358095E-15 ) ) ;
#1380=LINE ( 'NONE', #20835, #8973 ) ;
#1385=FACE_OUTER_BOUND ( 'NONE', #20347, .T. ) ;
#1388=CARTESIAN_POINT ( 'NONE',  ( 33.03948732994508930, 43.16218137147969003, 78.80433879953099563 ) ) ;
#1390=DIRECTION ( 'NONE',  ( 1.000000000000000000, 1.402518428993831183E-16, -4.865963288531424442E-32 ) ) ;
#1393=ORIENTED_EDGE ( 'NONE', *, *, #520, .T. ) ;
#1399=DIRECTION ( 'NONE',  ( -1.402518428993831183E-16, 1.000000000000000000, -3.469446951953617640E-16 ) ) ;
#1402=AXIS2_PLACEMENT_3D ( 'NONE', #17657, #12367, #18843 ) ;
#1424=EDGE_LOOP ( 'NONE', ( #5177, #9020, #16881, #15243 ) ) ;
#1467=EDGE_CURVE ( 'NONE', #4298, #3641, #18885, .T. ) ;
#1468=VERTEX_POINT ( 'NONE', #4293 ) ;
#1499=DIRECTION ( 'NONE',  ( -1.402518428993830937E-16, 1.000000000000000000, -3.469446951953617147E-16 ) ) ;
#1519=DIRECTION ( 'NONE',  ( -1.402518428993830937E-16, 1.000000000000000000, -3.469446951953617147E-16 ) ) ;
#1574=( NAMED_UNIT ( * ) SI_UNIT ( $, .STERADIAN. ) SOLID_ANGLE_UNIT ( ) );
#1600=VECTOR ( 'NONE', #16532, 1000.000000000000000 ) ;
#1622=DIRECTION ( 'NONE',  ( 1.000000000000000000, 0.000000000000000000, 0.000000000000000000 ) ) ;
#1743=CARTESIAN_POINT ( 'NONE',  ( 28.43948732994508077, 45.16218137147969003, 76.90433879953101837 ) ) ;
#1774=ORIENTED_EDGE ( 'NONE', *, *, #8570, .T. ) ;
#1775=DIRECTION ( 'NONE',  ( 6.308085367188358095E-15, 8.847205979147994320E-31, 1.000000000000000000 ) ) ;
#1777=ORIENTED_EDGE ( 'NONE', *, *, #1213, .T. ) ;
#1778=VECTOR ( 'NONE', #17685, 1000.000000000000000 ) ;
#1831=ORIENTED_EDGE ( 'NONE', *, *, #20566, .F. ) ;
#1844=EDGE_LOOP ( 'NONE', ( #10122, #11352, #17562, #17623 ) ) ;
#1855=CARTESIAN_POINT ( 'NONE',  ( 31.03948732994507864, 43.16218137147969003, 77.50433879953099847 ) ) ;
#1863=DIRECTION ( 'NONE',  ( -1.402518428993831183E-16, 1.000000000000000000, -3.469446951953617640E-16 ) ) ;
#1925=DIRECTION ( 'NONE',  ( 1.000000000000000000, 0.000000000000000000, 0.000000000000000000 ) ) ;
#2025=ORIENTED_EDGE ( 'NONE', *, *, #9304, .F. ) ;
#2035=DIRECTION ( 'NONE',  ( 6.308085367188358884E-15, 3.469446951953626515E-16, 1.000000000000000000 ) ) ;
#2039=EDGE_CURVE ( 'NONE', #16740, #7726, #5055, .T. ) ;
#2042=DIRECTION ( 'NONE',  ( 5.213532094855085691E-33, -3.469446951953617640E-16, -1.000000000000000000 ) ) ;
#2043=ORIENTED_EDGE ( 'NONE', *, *, #5556, .T. ) ;
#2044=CARTESIAN_POINT ( 'NONE',  ( 23.03948732994508575, 45.16218137147969003, 73.00433879953099847 ) ) ;
#2073=FACE_OUTER_BOUND ( 'NONE', #8920, .T. ) ;
#2120=CARTESIAN_POINT ( 'NONE',  ( 27.03948732994508219, 27.61837231449496244, 73.00433879953101268 ) ) ;
#2146=CARTESIAN_POINT ( 'NONE',  ( 24.43948732994508788, 43.16218137147969003, 74.70433879953100131 ) ) ;
#2153=LINE ( 'NONE', #8652, #16368 ) ;
#2174=AXIS2_PLACEMENT_3D ( 'NONE', #4794, #3000, #1622 ) ;
#2292=ORIENTED_EDGE ( 'NONE', *, *, #2813, .T. ) ;
#2300=ORIENTED_EDGE ( 'NONE', *, *, #14790, .T. ) ;
#2302=EDGE_CURVE ( 'NONE', #10971, #16740, #14912, .T. ) ;
#2316=DIRECTION ( 'NONE',  ( 1.402518428993831183E-16, -1.000000000000000000, 3.469446951953617640E-16 ) ) ;
#2321=FACE_OUTER_BOUND ( 'NONE', #11770, .T. ) ;
#2372=ORIENTED_EDGE ( 'NONE', *, *, #7430, .T. ) ;
#2393=ORIENTED_EDGE ( 'NONE', *, *, #2596, .T. ) ;
#2406=CARTESIAN_POINT ( 'NONE',  ( 25.03948732994508219, 43.16218137147969003, 74.70433879953100131 ) ) ;
#2409=PRODUCT_DEFINITION_FORMATION_WITH_SPECIFIED_SOURCE ( 'ANY', '', #3765, .NOT_KNOWN. ) ;
#2428=PLANE ( 'NONE',  #15528 ) ;
#2508=EDGE_LOOP ( 'NONE', ( #18283, #15086, #7600, #17745 ) ) ;
#2511=VERTEX_POINT ( 'NONE', #15211 ) ;
#2525=CARTESIAN_POINT ( 'NONE',  ( 29.63948732994508006, 45.16218137147968292, 74.70433879953100131 ) ) ;
#2547=LINE ( 'NONE', #5623, #20082 ) ;
#2555=ORIENTED_EDGE ( 'NONE', *, *, #15105, .T. ) ;
#2596=EDGE_CURVE ( 'NONE', #14483, #4403, #5297, .T. ) ;
#2615=AXIS2_PLACEMENT_3D ( 'NONE', #3207, #8205, #8098 ) ;
#2635=EDGE_CURVE ( 'NONE', #2902, #4298, #5758, .T. ) ;
#2651=CARTESIAN_POINT ( 'NONE',  ( 27.63948732994508006, 45.16218137147969003, 76.90433879953101837 ) ) ;
#2660=CARTESIAN_POINT ( 'NONE',  ( 23.03948732994508575, 45.16218137147969003, 78.60433879953099279 ) ) ;
#2680=PLANE ( 'NONE',  #8385 ) ;
#2686=CARTESIAN_POINT ( 'NONE',  ( 23.63948732994508717, 36.35905713404684292, 74.70433879953098710 ) ) ;
#2690=DIRECTION ( 'NONE',  ( 1.000000000000000000, 1.402518428993831183E-16, -4.344610079045915326E-32 ) ) ;
#2708=ORIENTED_EDGE ( 'NONE', *, *, #7274, .F. ) ;
#2712=ORIENTED_EDGE ( 'NONE', *, *, #17493, .F. ) ;
#2715=EDGE_LOOP ( 'NONE', ( #3482, #3305, #4945, #21020 ) ) ;
#2743=VERTEX_POINT ( 'NONE', #2651 ) ;
#2748=VECTOR ( 'NONE', #2035, 1000.000000000000000 ) ;
#2777=CIRCLE ( 'NONE', #1402, 1.399999999999995026 ) ;
#2786=CIRCLE ( 'NONE', #6173, 0.5999999999999928724 ) ;
#2794=CARTESIAN_POINT ( 'NONE',  ( 28.43948732994508788, 36.35905713404685002, 74.70433879953100131 ) ) ;
#2813=EDGE_CURVE ( 'NONE', #4756, #6140, #6430, .T. ) ;
#2818=AXIS2_PLACEMENT_3D ( 'NONE', #13477, #19854, #6773 ) ;
#2828=CARTESIAN_POINT ( 'NONE',  ( 30.43948732994509143, 36.35905713404685002, 76.90433879953101837 ) ) ;
#2877=EDGE_CURVE ( 'NONE', #5038, #9071, #4859, .T. ) ;
#2902=VERTEX_POINT ( 'NONE', #9572 ) ;
#2904=CARTESIAN_POINT ( 'NONE',  ( 23.03948732994508930, 27.61837231449496599, 76.90433879953101837 ) ) ;
#2922=ORIENTED_EDGE ( 'NONE', *, *, #4025, .F. ) ;
#2960=CYLINDRICAL_SURFACE ( 'NONE', #17049, 0.5999999999999894307 ) ;
#2979=VECTOR ( 'NONE', #11544, 1000.000000000000114 ) ;
#2981=EDGE_CURVE ( 'NONE', #6536, #16740, #13476, .T. ) ;
#3000=DIRECTION ( 'NONE',  ( 1.402518428993831183E-16, -1.000000000000000000, 3.469446951953617640E-16 ) ) ;
#3034=EDGE_CURVE ( 'NONE', #9780, #14257, #9993, .T. ) ;
#3055=AXIS2_PLACEMENT_3D ( 'NONE', #15100, #11707, #5513 ) ;
#3058=SURFACE_STYLE_USAGE ( .BOTH. , #4637 ) ;
#3059=DIRECTION ( 'NONE',  ( 0.000000000000000000, -1.000000000000000000, 3.469446951953617147E-16 ) ) ;
#3061=DIRECTION ( 'NONE',  ( 1.000000000000000000, 0.000000000000000000, 0.000000000000000000 ) ) ;
#3092=FACE_OUTER_BOUND ( 'NONE', #3618, .T. ) ;
#3101=LINE ( 'NONE', #2794, #9744 ) ;
#3146=CARTESIAN_POINT ( 'NONE',  ( 29.63948732994508006, 43.16218137147969003, 74.70433879953100131 ) ) ;
#3149=VERTEX_POINT ( 'NONE', #2525 ) ;
#3151=LINE ( 'NONE', #9652, #7815 ) ;
#3184=ORIENTED_EDGE ( 'NONE', *, *, #5323, .F. ) ;
#3201=DIRECTION ( 'NONE',  ( 1.000000000000000000, 0.000000000000000000, 0.000000000000000000 ) ) ;
#3207=CARTESIAN_POINT ( 'NONE',  ( 9.539487329945091076, 44.16218137147970424, 95.45352954694192249 ) ) ;
#3228=EDGE_CURVE ( 'NONE', #3149, #11295, #6225, .T. ) ;
#3277=EDGE_CURVE ( 'NONE', #11695, #7082, #3151, .T. ) ;
#3285=DIRECTION ( 'NONE',  ( 0.7071067811865460184, 0.000000000000000000, 0.7071067811865490160 ) ) ;
#3305=ORIENTED_EDGE ( 'NONE', *, *, #20668, .T. ) ;
#3341=CIRCLE ( 'NONE', #15245, 1.000000000000014655 ) ;
#3348=CARTESIAN_POINT ( 'NONE',  ( 23.03948732994508575, 36.35905713404685002, 76.90433879953101837 ) ) ;
#3360=CARTESIAN_POINT ( 'NONE',  ( 24.43948732994508077, 45.16218137147969003, 76.90433879953101837 ) ) ;
#3452=DIRECTION ( 'NONE',  ( -1.402518428993831676E-16, 1.000000000000000000, -0.000000000000000000 ) ) ;
#3482=ORIENTED_EDGE ( 'NONE', *, *, #13035, .F. ) ;
#3492=ADVANCED_FACE ( 'NONE', ( #2073 ), #8569, .F. ) ;
#3508=ADVANCED_FACE ( 'NONE', ( #8357 ), #14838, .F. ) ;
#3611=ADVANCED_FACE ( 'NONE', ( #7379 ), #1113, .T. ) ;
#3618=EDGE_LOOP ( 'NONE', ( #17612, #2292, #17204, #2712, #16419, #11428, #1030, #1138, #15911, #2708, #5101, #9805, #14390, #2922, #1232, #9621, #215, #17593, #3635, #8013, #19207, #16743, #17505, #6878, #10617, #143, #9563, #2300 ) ) ;
#3622=LINE ( 'NONE', #10131, #2748 ) ;
#3629=ORIENTED_EDGE ( 'NONE', *, *, #6765, .F. ) ;
#3635=ORIENTED_EDGE ( 'NONE', *, *, #20158, .F. ) ;
#3641=VERTEX_POINT ( 'NONE', #5790 ) ;
#3642=ADVANCED_FACE ( 'NONE', ( #10716 ), #12397, .T. ) ;
#3690=CARTESIAN_POINT ( 'NONE',  ( 30.43948732994509143, 45.16218137147969003, 76.90433879953101837 ) ) ;
#3697=DIRECTION ( 'NONE',  ( 0.000000000000000000, 0.000000000000000000, 1.000000000000000000 ) ) ;
#3723=DIRECTION ( 'NONE',  ( -1.402518428993831183E-16, 1.000000000000000000, -3.469446951953617640E-16 ) ) ;
#3725=ADVANCED_FACE ( 'NONE', ( #20964 ), #12904, .F. ) ;
#3755=LINE ( 'NONE', #55, #9847 ) ;
#3765=PRODUCT ( 'Locking Springs', 'Locking Springs', '', ( #4206 ) ) ;
#3767=ORIENTED_EDGE ( 'NONE', *, *, #20265, .F. ) ;
#3770=VERTEX_POINT ( 'NONE', #1743 ) ;
#3780=DIRECTION ( 'NONE',  ( 1.000000000000000000, 0.000000000000000000, 0.000000000000000000 ) ) ;
#3787=ORIENTED_EDGE ( 'NONE', *, *, #5556, .F. ) ;
#3809=DIRECTION ( 'NONE',  ( 0.000000000000000000, 1.000000000000000000, -3.469446951953617147E-16 ) ) ;
#3828=CARTESIAN_POINT ( 'NONE',  ( 31.03948732994507864, 43.16218137147969003, 78.30433879953099563 ) ) ;
#3836=EDGE_CURVE ( 'NONE', #3641, #3770, #14256, .T. ) ;
#3866=VERTEX_POINT ( 'NONE', #8542 ) ;
#3928=VERTEX_POINT ( 'NONE', #15136 ) ;
#3930=CARTESIAN_POINT ( 'NONE',  ( 8.832380548758539618, 43.45507459029313679, 73.00433879953099847 ) ) ;
#3992=VECTOR ( 'NONE', #17217, 1000.000000000000000 ) ;
#4025=EDGE_CURVE ( 'NONE', #18137, #14483, #1088, .T. ) ;
#4026=CARTESIAN_POINT ( 'NONE',  ( 23.03948732994508575, 45.16218137147969003, 78.30433879953099563 ) ) ;
#4029=ADVANCED_FACE ( 'NONE', ( #20941 ), #11091, .T. ) ;
#4038=CARTESIAN_POINT ( 'NONE',  ( 27.03948732994508930, 43.16218137147969003, 77.50433879953099847 ) ) ;
#4066=LINE ( 'NONE', #2686, #20328 ) ;
#4080=CARTESIAN_POINT ( 'NONE',  ( 29.63948732994508006, 36.35905713404685002, 74.70433879953100131 ) ) ;
#4108=DIRECTION ( 'NONE',  ( 0.000000000000000000, 3.469446951953617147E-16, 1.000000000000000000 ) ) ;
#4114=CYLINDRICAL_SURFACE ( 'NONE', #4966, 0.6000000000000033085 ) ;
#4127=VECTOR ( 'NONE', #4811, 1000.000000000000000 ) ;
#4157=VECTOR ( 'NONE', #16710, 1000.000000000000000 ) ;
#4161=AXIS2_PLACEMENT_3D ( 'NONE', #611, #20397, #10430 ) ;
#4177=DIRECTION ( 'NONE',  ( 0.000000000000000000, -1.000000000000000000, 0.000000000000000000 ) ) ;
#4205=CIRCLE ( 'NONE', #16103, 0.5999999999999928724 ) ;
#4206=PRODUCT_CONTEXT ( 'NONE', #435, 'mechanical' ) ;
#4282=AXIS2_PLACEMENT_3D ( 'NONE', #16999, #7202, #10427 ) ;
#4290=DIRECTION ( 'NONE',  ( 0.7071067811865460184, 3.444999758574045180E-16, 0.7071067811865490160 ) ) ;
#4293=CARTESIAN_POINT ( 'NONE',  ( 13.13948732994505875, 43.16218137147969003, 78.60433879953099279 ) ) ;
#4298=VERTEX_POINT ( 'NONE', #5099 ) ;
#4300=CARTESIAN_POINT ( 'NONE',  ( 29.03948732994507864, 36.35905713404685002, 74.70433879953100131 ) ) ;
#4301=EDGE_CURVE ( 'NONE', #1145, #13369, #5102, .T. ) ;
#4333=VECTOR ( 'NONE', #14643, 1000.000000000000000 ) ;
#4353=VERTEX_POINT ( 'NONE', #10017 ) ;
#4391=VECTOR ( 'NONE', #20805, 1000.000000000000114 ) ;
#4393=LINE ( 'NONE', #17388, #17756 ) ;
#4403=VERTEX_POINT ( 'NONE', #4026 ) ;
#4418=AXIS2_PLACEMENT_3D ( 'NONE', #4080, #15480, #7493 ) ;
#4447=CARTESIAN_POINT ( 'NONE',  ( 31.03948732994507864, 43.16218137147969003, 76.90433879953100416 ) ) ;
#4462=CARTESIAN_POINT ( 'NONE',  ( 31.03948732994507864, 36.35905713404685002, 76.90433879953100416 ) ) ;
#4470=AXIS2_PLACEMENT_3D ( 'NONE', #14388, #12897, #20861 ) ;
#4481=ORIENTED_EDGE ( 'NONE', *, *, #5592, .F. ) ;
#4542=FACE_OUTER_BOUND ( 'NONE', #13893, .T. ) ;
#4554=VERTEX_POINT ( 'NONE', #9862 ) ;
#4562=DIRECTION ( 'NONE',  ( 0.000000000000000000, 0.000000000000000000, 1.000000000000000000 ) ) ;
#4563=EDGE_CURVE ( 'NONE', #18617, #10971, #16345, .T. ) ;
#4570=CARTESIAN_POINT ( 'NONE',  ( 23.03948732994508575, 43.16218137147969003, 76.90433879953101837 ) ) ;
#4572=ORIENTED_EDGE ( 'NONE', *, *, #2635, .T. ) ;
#4581=VERTEX_POINT ( 'NONE', #5044 ) ;
#4583=EDGE_CURVE ( 'NONE', #1468, #18137, #5252, .T. ) ;
#4625=ORIENTED_EDGE ( 'NONE', *, *, #1213, .F. ) ;
#4627=CARTESIAN_POINT ( 'NONE',  ( 8.832380548758539618, 43.45507459029313679, 73.00433879953099847 ) ) ;
#4637=SURFACE_SIDE_STYLE ('',( #12744 ) ) ;
#4647=DIRECTION ( 'NONE',  ( 0.000000000000000000, 0.000000000000000000, 1.000000000000000000 ) ) ;
#4664=DIRECTION ( 'NONE',  ( -1.402518428993831183E-16, 1.000000000000000000, 0.000000000000000000 ) ) ;
#4691=ORIENTED_EDGE ( 'NONE', *, *, #15958, .F. ) ;
#4743=DIRECTION ( 'NONE',  ( -1.402518428993831183E-16, 1.000000000000000000, -3.469446951953617640E-16 ) ) ;
#4744=AXIS2_PLACEMENT_3D ( 'NONE', #18215, #29, #6608 ) ;
#4756=VERTEX_POINT ( 'NONE', #6168 ) ;
#4765=ADVANCED_FACE ( 'NONE', ( #3092 ), #11087, .T. ) ;
#4784=EDGE_CURVE ( 'NONE', #2902, #7082, #9799, .T. ) ;
#4794=CARTESIAN_POINT ( 'NONE',  ( 25.03948732994508219, 45.16218137147969003, 74.70433879953100131 ) ) ;
#4803=CARTESIAN_POINT ( 'NONE',  ( 26.43948732994507367, 36.35905713404684292, 74.70433879953098710 ) ) ;
#4811=DIRECTION ( 'NONE',  ( 5.213532094855085691E-33, -3.469446951953617640E-16, -1.000000000000000000 ) ) ;
#4854=CARTESIAN_POINT ( 'NONE',  ( 29.03948732994507864, 43.16218137147969003, 74.70433879953100131 ) ) ;
#4859=LINE ( 'NONE', #17957, #17648 ) ;
#4876=VERTEX_POINT ( 'NONE', #14783 ) ;
#4900=DIRECTION ( 'NONE',  ( 1.000000000000000000, 0.000000000000000000, 0.000000000000000000 ) ) ;
#4903=EDGE_LOOP ( 'NONE', ( #41, #1774, #515, #2025 ) ) ;
#4945=ORIENTED_EDGE ( 'NONE', *, *, #9687, .T. ) ;
#4966=AXIS2_PLACEMENT_3D ( 'NONE', #18702, #17527, #5935 ) ;
#4975=FACE_OUTER_BOUND ( 'NONE', #1424, .T. ) ;
#4984=DIRECTION ( 'NONE',  ( 1.000000000000000000, 1.402518428993831676E-16, 0.000000000000000000 ) ) ;
#4998=LINE ( 'NONE', #13208, #20300 ) ;
#5012=LINE ( 'NONE', #9725, #393 ) ;
#5032=DIRECTION ( 'NONE',  ( 3.154042683594179047E-15, 0.000000000000000000, -1.000000000000000000 ) ) ;
#5038=VERTEX_POINT ( 'NONE', #17534 ) ;
#5044=CARTESIAN_POINT ( 'NONE',  ( 9.539487329945080418, 45.16218137147970424, 73.00433879953099847 ) ) ;
#5055=CIRCLE ( 'NONE', #9494, 0.5999999999999928724 ) ;
#5074=ORIENTED_EDGE ( 'NONE', *, *, #7153, .T. ) ;
#5087=AXIS2_PLACEMENT_3D ( 'NONE', #10496, #10390, #16859 ) ;
#5093=ORIENTED_EDGE ( 'NONE', *, *, #18272, .F. ) ;
#5099=CARTESIAN_POINT ( 'NONE',  ( 27.03948732994508930, 43.16218137147969003, 78.30433879953100984 ) ) ;
#5101=ORIENTED_EDGE ( 'NONE', *, *, #7430, .F. ) ;
#5102=CIRCLE ( 'NONE', #8167, 1.399999999999995026 ) ;
#5157=DIRECTION ( 'NONE',  ( 3.154042683594179442E-15, -3.469446951953613203E-16, -1.000000000000000000 ) ) ;
#5177=ORIENTED_EDGE ( 'NONE', *, *, #2877, .F. ) ;
#5251=VERTEX_POINT ( 'NONE', #8354 ) ;
#5252=LINE ( 'NONE', #13148, #19052 ) ;
#5254=ORIENTED_EDGE ( 'NONE', *, *, #13035, .T. ) ;
#5269=ORIENTED_EDGE ( 'NONE', *, *, #12803, .F. ) ;
#5279=EDGE_CURVE ( 'NONE', #14483, #9281, #7101, .T. ) ;
#5297=LINE ( 'NONE', #17894, #6085 ) ;
#5323=EDGE_CURVE ( 'NONE', #11825, #4581, #3755, .T. ) ;
#5379=DIRECTION ( 'NONE',  ( 1.402518428993831183E-16, -1.000000000000000000, 3.469446951953617640E-16 ) ) ;
#5393=LINE ( 'NONE', #20077, #11219 ) ;
#5482=VECTOR ( 'NONE', #2042, 1000.000000000000000 ) ;
#5494=VECTOR ( 'NONE', #19305, 1000.000000000000000 ) ;
#5505=DIRECTION ( 'NONE',  ( 3.154042683594179442E-15, -3.469446951953613203E-16, -1.000000000000000000 ) ) ;
#5506=DIRECTION ( 'NONE',  ( 1.402518428993831183E-16, -1.000000000000000000, 3.469446951953617640E-16 ) ) ;
#5508=FACE_OUTER_BOUND ( 'NONE', #20974, .T. ) ;
#5513=DIRECTION ( 'NONE',  ( 3.154042683594179442E-15, 0.000000000000000000, -1.000000000000000000 ) ) ;
#5534=CARTESIAN_POINT ( 'NONE',  ( 27.63948732994508006, 45.16218137147969003, 76.90433879953101837 ) ) ;
#5556=EDGE_CURVE ( 'NONE', #14081, #8173, #20070, .T. ) ;
#5565=LINE ( 'NONE', #12067, #10459 ) ;
#5588=APPLICATION_CONTEXT ( 'automotive_design' ) ;
#5592=EDGE_CURVE ( 'NONE', #8992, #2511, #12328, .T. ) ;
#5608=CARTESIAN_POINT ( 'NONE',  ( 24.43948732994508788, 36.35905713404684292, 74.70433879953100131 ) ) ;
#5623=CARTESIAN_POINT ( 'NONE',  ( 25.63948732994507651, 36.35905713404684292, 74.70433879953100131 ) ) ;
#5653=VECTOR ( 'NONE', #12759, 1000.000000000000000 ) ;
#5676=DIRECTION ( 'NONE',  ( 1.000000000000000000, 0.000000000000000000, 0.000000000000000000 ) ) ;
#5683=VECTOR ( 'NONE', #14854, 1000.000000000000000 ) ;
#5685=ORIENTED_EDGE ( 'NONE', *, *, #20566, .T. ) ;
#5691=DIRECTION ( 'NONE',  ( -1.402518428993831183E-16, 1.000000000000000000, -3.469446951953617640E-16 ) ) ;
#5710=ADVANCED_FACE ( 'NONE', ( #14850 ), #6655, .T. ) ;
#5720=EDGE_CURVE ( 'NONE', #5251, #1145, #13057, .T. ) ;
#5758=CIRCLE ( 'NONE', #19347, 1.399999999999995026 ) ;
#5768=DIRECTION ( 'NONE',  ( 3.154042683594179047E-15, 4.423602989573997160E-31, -1.000000000000000000 ) ) ;
#5774=VERTEX_POINT ( 'NONE', #8474 ) ;
#5775=DIRECTION ( 'NONE',  ( -1.402518428993830937E-16, 1.000000000000000000, -3.469446951953617147E-16 ) ) ;
#5790=CARTESIAN_POINT ( 'NONE',  ( 27.03948732994508930, 45.16218137147969003, 78.30433879953100984 ) ) ;
#5810=EDGE_CURVE ( 'NONE', #3928, #2511, #19936, .T. ) ;
#5828=LINE ( 'NONE', #9251, #427 ) ;
#5842=FACE_OUTER_BOUND ( 'NONE', #18379, .T. ) ;
#5856=LINE ( 'NONE', #16824, #10322 ) ;
#5869=AXIS2_PLACEMENT_3D ( 'NONE', #933, #18597, #9140 ) ;
#5915=CARTESIAN_POINT ( 'NONE',  ( 23.03948732994508575, 43.16218137147968292, 76.90433879953101837 ) ) ;
#5920=CARTESIAN_POINT ( 'NONE',  ( 31.03948732994507864, 45.16218137147969003, 78.30433879953099563 ) ) ;
#5935=DIRECTION ( 'NONE',  ( 0.000000000000000000, 0.000000000000000000, 1.000000000000000000 ) ) ;
#5951=LINE ( 'NONE', #12450, #5653 ) ;
#5986=CARTESIAN_POINT ( 'NONE',  ( 9.125273767571991712, 43.16218137147968292, 75.00433879953099847 ) ) ;
#5995=DIRECTION ( 'NONE',  ( 6.308085367188358095E-15, 0.000000000000000000, 1.000000000000000000 ) ) ;
#6048=AXIS2_PLACEMENT_3D ( 'NONE', #4462, #17350, #4562 ) ;
#6085=VECTOR ( 'NONE', #10114, 1000.000000000000000 ) ;
#6090=ORIENTED_EDGE ( 'NONE', *, *, #11173, .F. ) ;
#6103=VECTOR ( 'NONE', #13886, 1000.000000000000000 ) ;
#6109=CYLINDRICAL_SURFACE ( 'NONE', #15293, 1.399999999999998579 ) ;
#6140=VERTEX_POINT ( 'NONE', #1855 ) ;
#6168=CARTESIAN_POINT ( 'NONE',  ( 30.43948732994509143, 43.16218137147969003, 76.90433879953101837 ) ) ;
#6173=AXIS2_PLACEMENT_3D ( 'NONE', #13898, #20382, #15613 ) ;
#6205=AXIS2_PLACEMENT_3D ( 'NONE', #798, #20247, #5676 ) ;
#6225=LINE ( 'NONE', #16030, #9861 ) ;
#6257=ORIENTED_EDGE ( 'NONE', *, *, #12803, .T. ) ;
#6259=CARTESIAN_POINT ( 'NONE',  ( 29.63948732994508006, 45.16218137147969003, 76.90433879953101837 ) ) ;
#6261=DIRECTION ( 'NONE',  ( 1.000000000000000000, 1.402518428993831676E-16, -4.865963288531424989E-32 ) ) ;
#6273=DIRECTION ( 'NONE',  ( -4.344610079045915326E-32, -6.093395702654244599E-48, -1.000000000000000000 ) ) ;
#6322=CARTESIAN_POINT ( 'NONE',  ( 30.43948732994507722, 36.35905713404685002, 74.70433879953098710 ) ) ;
#6339=CARTESIAN_POINT ( 'NONE',  ( 25.63948732994507651, 45.16218137147968292, 74.70433879953100131 ) ) ;
#6349=VECTOR ( 'NONE', #13830, 1000.000000000000000 ) ;
#6393=CARTESIAN_POINT ( 'NONE',  ( 24.43948732994508077, 43.16218137147969003, 76.90433879953101837 ) ) ;
#6418=CARTESIAN_POINT ( 'NONE',  ( 29.63948732994508006, 36.35905713404685002, 74.70433879953100131 ) ) ;
#6430=CIRCLE ( 'NONE', #16971, 0.5999999999999998668 ) ;
#6484=ORIENTED_EDGE ( 'NONE', *, *, #1467, .F. ) ;
#6506=EDGE_CURVE ( 'NONE', #20749, #2743, #4998, .T. ) ;
#6507=EDGE_LOOP ( 'NONE', ( #13339, #10070, #18530, #18532 ) ) ;
#6536=VERTEX_POINT ( 'NONE', #16191 ) ;
#6562=DIRECTION ( 'NONE',  ( -1.402518428993831183E-16, 1.000000000000000000, -3.469446951953617640E-16 ) ) ;
#6589=ORIENTED_EDGE ( 'NONE', *, *, #17493, .T. ) ;
#6608=DIRECTION ( 'NONE',  ( 1.000000000000000000, 0.000000000000000000, 0.000000000000000000 ) ) ;
#6648=VERTEX_POINT ( 'NONE', #4038 ) ;
#6655=CYLINDRICAL_SURFACE ( 'NONE', #7824, 1.399999999999998579 ) ;
#6679=DIRECTION ( 'NONE',  ( -0.7071067811865490160, 1.461539174812751569E-16, 0.7071067811865460184 ) ) ;
#6700=FACE_OUTER_BOUND ( 'NONE', #6507, .T. ) ;
#6707=VECTOR ( 'NONE', #14362, 1000.000000000000000 ) ;
#6730=CARTESIAN_POINT ( 'NONE',  ( 27.03948732994508930, 36.35905713404685713, 77.50433879953099847 ) ) ;
#6765=EDGE_CURVE ( 'NONE', #18137, #19468, #10874, .T. ) ;
#6772=EDGE_CURVE ( 'NONE', #8020, #11255, #17235, .T. ) ;
#6773=DIRECTION ( 'NONE',  ( 0.000000000000000000, 0.000000000000000000, 1.000000000000000000 ) ) ;
#6777=ORIENTED_EDGE ( 'NONE', *, *, #13480, .T. ) ;
#6823=ORIENTED_EDGE ( 'NONE', *, *, #18272, .T. ) ;
#6878=ORIENTED_EDGE ( 'NONE', *, *, #4563, .T. ) ;
#6879=DIRECTION ( 'NONE',  ( -1.402518428993831183E-16, 1.000000000000000000, -3.469446951953617640E-16 ) ) ;
#6881=CARTESIAN_POINT ( 'NONE',  ( 29.03948732994507864, 45.16218137147969003, 74.70433879953100131 ) ) ;
#6948=DIRECTION ( 'NONE',  ( -1.402518428993830937E-16, 1.000000000000000000, -3.469446951953617147E-16 ) ) ;
#6958=ORIENTED_EDGE ( 'NONE', *, *, #10062, .F. ) ;
#6987=DIRECTION ( 'NONE',  ( 4.150711087041459392E-32, -3.469446951953617147E-16, -1.000000000000000000 ) ) ;
#7005=LINE ( 'NONE', #8637, #19339 ) ;
#7016=CARTESIAN_POINT ( 'NONE',  ( 28.43948732994508077, 43.16218137147969003, 76.90433879953101837 ) ) ;
#7021=UNCERTAINTY_MEASURE_WITH_UNIT (LENGTH_MEASURE( 1.000000000000000082E-05 ), #16252, 'distance_accuracy_value', 'NONE');
#7027=COLOUR_RGB ( '', 0.72549020, 0.75294118, 0.79215686) ;
#7082=VERTEX_POINT ( 'NONE', #20607 ) ;
#7101=CIRCLE ( 'NONE', #19017, 1.399999999999995026 ) ;
#7108=VECTOR ( 'NONE', #8786, 1000.000000000000000 ) ;
#7113=CIRCLE ( 'NONE', #18685, 1.399999999999995026 ) ;
#7124=CARTESIAN_POINT ( 'NONE',  ( 31.03948732994507864, 45.16218137147969003, 76.90433879953100416 ) ) ;
#7148=VECTOR ( 'NONE', #14898, 1000.000000000000000 ) ;
#7153=EDGE_CURVE ( 'NONE', #6140, #5774, #12536, .T. ) ;
#7202=DIRECTION ( 'NONE',  ( -1.402518428993831676E-16, 1.000000000000000000, -0.000000000000000000 ) ) ;
#7224=LINE ( 'NONE', #10343, #4157 ) ;
#7235=EDGE_CURVE ( 'NONE', #16996, #8020, #242, .T. ) ;
#7239=CARTESIAN_POINT ( 'NONE',  ( 9.539487329945080418, 45.16218137147970424, 75.00433879953099847 ) ) ;
#7255=CARTESIAN_POINT ( 'NONE',  ( 23.63948732994508006, 43.16218137147968292, 76.90433879953101837 ) ) ;
#7263=CARTESIAN_POINT ( 'NONE',  ( 23.03948732994508575, 43.16218137147968292, 77.50433879953099847 ) ) ;
#7274=EDGE_CURVE ( 'NONE', #4353, #2902, #13860, .T. ) ;
#7286=CARTESIAN_POINT ( 'NONE',  ( 23.03948732994508575, 45.16218137147969003, 77.50433879953099847 ) ) ;
#7310=PLANE ( 'NONE',  #18452 ) ;
#7379=FACE_OUTER_BOUND ( 'NONE', #1844, .T. ) ;
#7388=FACE_OUTER_BOUND ( 'NONE', #1040, .T. ) ;
#7420=FACE_OUTER_BOUND ( 'NONE', #13797, .T. ) ;
#7430=EDGE_CURVE ( 'NONE', #8992, #4353, #14203, .T. ) ;
#7462=ORIENTED_EDGE ( 'NONE', *, *, #19641, .T. ) ;
#7477=ORIENTED_EDGE ( 'NONE', *, *, #20414, .T. ) ;
#7493=DIRECTION ( 'NONE',  ( 6.308085367188358884E-15, 0.000000000000000000, 1.000000000000000000 ) ) ;
#7504=ORIENTED_EDGE ( 'NONE', *, *, #1467, .T. ) ;
#7545=FACE_OUTER_BOUND ( 'NONE', #15884, .T. ) ;
#7594=PLANE ( 'NONE',  #11014 ) ;
#7600=ORIENTED_EDGE ( 'NONE', *, *, #901, .T. ) ;
#7628=DIRECTION ( 'NONE',  ( -1.402518428993831183E-16, 1.000000000000000000, -3.469446951953617640E-16 ) ) ;
#7646=ADVANCED_FACE ( 'NONE', ( #1385 ), #10877, .T. ) ;
#7678=SHAPE_REPRESENTATION ( 'Locking Springs', ( #18366 ), #9896 ) ;
#7694=EDGE_CURVE ( 'NONE', #1468, #3866, #7983, .T. ) ;
#7726=VERTEX_POINT ( 'NONE', #14573 ) ;
#7735=LINE ( 'NONE', #4627, #4391 ) ;
#7755=CARTESIAN_POINT ( 'NONE',  ( 25.63948732994507651, 36.35905713404684292, 74.70433879953100131 ) ) ;
#7774=PLANE ( 'NONE',  #14998 ) ;
#7777=DIRECTION ( 'NONE',  ( -1.402518428993831183E-16, 1.000000000000000000, -3.469446951953617640E-16 ) ) ;
#7802=AXIS2_PLACEMENT_3D ( 'NONE', #2120, #6987, #3809 ) ;
#7813=CIRCLE ( 'NONE', #14614, 0.5999999999999928724 ) ;
#7815=VECTOR ( 'NONE', #16135, 1000.000000000000000 ) ;
#7818=VERTEX_POINT ( 'NONE', #11396 ) ;
#7824=AXIS2_PLACEMENT_3D ( 'NONE', #16353, #19632, #16558 ) ;
#7826=EDGE_CURVE ( 'NONE', #13483, #11825, #9556, .T. ) ;
#7847=CARTESIAN_POINT ( 'NONE',  ( 26.43948732994507367, 36.35905713404684292, 74.70433879953098710 ) ) ;
#7912=AXIS2_PLACEMENT_3D ( 'NONE', #8118, #14501, #135 ) ;
#7983=LINE ( 'NONE', #10773, #9470 ) ;
#8013=ORIENTED_EDGE ( 'NONE', *, *, #8, .F. ) ;
#8020=VERTEX_POINT ( 'NONE', #16661 ) ;
#8074=ADVANCED_FACE ( 'NONE', ( #7388 ), #13674, .F. ) ;
#8098=DIRECTION ( 'NONE',  ( 0.000000000000000000, 1.000000000000000000, 0.000000000000000000 ) ) ;
#8118=CARTESIAN_POINT ( 'NONE',  ( 27.03948732994508930, 45.16218137147969003, 76.90433879953101837 ) ) ;
#8152=VERTEX_POINT ( 'NONE', #7286 ) ;
#8156=AXIS2_PLACEMENT_3D ( 'NONE', #10535, #15419, #3697 ) ;
#8167=AXIS2_PLACEMENT_3D ( 'NONE', #11816, #8195, #3201 ) ;
#8171=FACE_OUTER_BOUND ( 'NONE', #14492, .T. ) ;
#8173=VERTEX_POINT ( 'NONE', #11873 ) ;
#8195=DIRECTION ( 'NONE',  ( 1.402518428993831183E-16, -1.000000000000000000, 3.469446951953617640E-16 ) ) ;
#8202=VECTOR ( 'NONE', #13072, 1000.000000000000000 ) ;
#8205=DIRECTION ( 'NONE',  ( 5.731934358295347564E-32, -3.469446951953617147E-16, -1.000000000000000000 ) ) ;
#8262=ORIENTED_EDGE ( 'NONE', *, *, #17953, .T. ) ;
#8266=PRODUCT_DEFINITION_CONTEXT ( 'detailed design', #5588, 'design' ) ;
#8270=CARTESIAN_POINT ( 'NONE',  ( 27.03948732994508219, 43.16218137147969003, 73.00433879953099847 ) ) ;
#8287=ORIENTED_EDGE ( 'NONE', *, *, #5720, .F. ) ;
#8354=CARTESIAN_POINT ( 'NONE',  ( 27.63948732994508717, 43.16218137147969003, 74.70433879953098710 ) ) ;
#8356=ORIENTED_EDGE ( 'NONE', *, *, #2981, .T. ) ;
#8357=FACE_OUTER_BOUND ( 'NONE', #14761, .T. ) ;
#8371=LINE ( 'NONE', #11577, #5683 ) ;
#8379=ORIENTED_EDGE ( 'NONE', *, *, #18296, .T. ) ;
#8385=AXIS2_PLACEMENT_3D ( 'NONE', #19068, #20549, #9187 ) ;
#8413=MECHANICAL_DESIGN_GEOMETRIC_PRESENTATION_REPRESENTATION('',(#9444),#19937);
#8456=ORIENTED_EDGE ( 'NONE', *, *, #3034, .F. ) ;
#8474=CARTESIAN_POINT ( 'NONE',  ( 31.03948732994507864, 45.16218137147969003, 77.50433879953099847 ) ) ;
#8492=DIRECTION ( 'NONE',  ( 1.000000000000000000, 0.000000000000000000, 0.000000000000000000 ) ) ;
#8533=ORIENTED_EDGE ( 'NONE', *, *, #10703, .T. ) ;
#8542=CARTESIAN_POINT ( 'NONE',  ( 13.13948732994505875, 45.16218137147969003, 78.60433879953099279 ) ) ;
#8569=CYLINDRICAL_SURFACE ( 'NONE', #674, 0.5999999999999894307 ) ;
#8570=EDGE_CURVE ( 'NONE', #15837, #8173, #4066, .T. ) ;
#8590=EDGE_CURVE ( 'NONE', #4581, #11255, #3341, .T. ) ;
#8609=DIRECTION ( 'NONE',  ( 0.000000000000000000, -1.000000000000000000, 3.469446951953617147E-16 ) ) ;
#8613=CARTESIAN_POINT ( 'NONE',  ( 25.03948732994508219, 45.16218137147969003, 74.70433879953100131 ) ) ;
#8637=CARTESIAN_POINT ( 'NONE',  ( 9.125273767571993488, 43.16218137147969713, 95.45352954694192249 ) ) ;
#8652=CARTESIAN_POINT ( 'NONE',  ( 27.03948732994508219, 45.16218137147969003, 78.60433879953099279 ) ) ;
#8701=ORIENTED_EDGE ( 'NONE', *, *, #20704, .F. ) ;
#8707=ORIENTED_EDGE ( 'NONE', *, *, #768, .F. ) ;
#8768=DIRECTION ( 'NONE',  ( 6.308085367188358095E-15, 8.847205979147994320E-31, 1.000000000000000000 ) ) ;
#8786=DIRECTION ( 'NONE',  ( -1.402518428993831183E-16, 1.000000000000000000, -3.469446951953617640E-16 ) ) ;
#8817=PLANE ( 'NONE',  #3055 ) ;
#8857=PRODUCT_DEFINITION ( 'UNKNOWN', '', #2409, #8266 ) ;
#8920=EDGE_LOOP ( 'NONE', ( #3767, #17605, #7462, #82 ) ) ;
#8973=VECTOR ( 'NONE', #6261, 1000.000000000000000 ) ;
#8978=ORIENTED_EDGE ( 'NONE', *, *, #6506, .F. ) ;
#8990=ORIENTED_EDGE ( 'NONE', *, *, #5810, .T. ) ;
#8992=VERTEX_POINT ( 'NONE', #2146 ) ;
#9010=DIRECTION ( 'NONE',  ( 1.402518428993831676E-16, -1.000000000000000000, 0.000000000000000000 ) ) ;
#9020=ORIENTED_EDGE ( 'NONE', *, *, #17009, .T. ) ;
#9024=ORIENTED_EDGE ( 'NONE', *, *, #3836, .T. ) ;
#9071=VERTEX_POINT ( 'NONE', #7239 ) ;
#9085=ADVANCED_BREP_SHAPE_REPRESENTATION ( '', ( #11671, #18366 ), #9896 ) ;
#9140=DIRECTION ( 'NONE',  ( 6.308085367188358884E-15, 0.000000000000000000, 1.000000000000000000 ) ) ;
#9167=DIRECTION ( 'NONE',  ( -1.402518428993831183E-16, 1.000000000000000000, -3.469446951953617147E-16 ) ) ;
#9169=VECTOR ( 'NONE', #12215, 1000.000000000000000 ) ;
#9174=VERTEX_POINT ( 'NONE', #3690 ) ;
#9187=DIRECTION ( 'NONE',  ( -0.7071067811865506814, 0.7071067811865443531, 0.000000000000000000 ) ) ;
#9251=CARTESIAN_POINT ( 'NONE',  ( 9.539487329945080418, 45.16218137147971845, 95.45352954694192249 ) ) ;
#9281=VERTEX_POINT ( 'NONE', #20808 ) ;
#9304=EDGE_CURVE ( 'NONE', #18617, #6536, #17522, .T. ) ;
#9309=ORIENTED_EDGE ( 'NONE', *, *, #3228, .F. ) ;
#9332=FACE_OUTER_BOUND ( 'NONE', #13391, .T. ) ;
#9444=STYLED_ITEM ( 'NONE', ( #20908 ), #11671 ) ;
#9459=( NAMED_UNIT ( * ) PLANE_ANGLE_UNIT ( ) SI_UNIT ( $, .RADIAN. ) );
#9470=VECTOR ( 'NONE', #9167, 1000.000000000000000 ) ;
#9494=AXIS2_PLACEMENT_3D ( 'NONE', #12654, #6562, #11687 ) ;
#9499=EDGE_CURVE ( 'NONE', #4554, #15837, #16738, .T. ) ;
#9531=ORIENTED_EDGE ( 'NONE', *, *, #18748, .T. ) ;
#9555=AXIS2_PLACEMENT_3D ( 'NONE', #1388, #13089, #4984 ) ;
#9556=LINE ( 'NONE', #14215, #19957 ) ;
#9563=ORIENTED_EDGE ( 'NONE', *, *, #15958, .T. ) ;
#9565=( NAMED_UNIT ( * ) PLANE_ANGLE_UNIT ( ) SI_UNIT ( $, .RADIAN. ) );
#9572=CARTESIAN_POINT ( 'NONE',  ( 25.63948732994508362, 43.16218137147969003, 76.90433879953101837 ) ) ;
#9621=ORIENTED_EDGE ( 'NONE', *, *, #17009, .F. ) ;
#9632=ADVANCED_FACE ( 'NONE', ( #12379 ), #2680, .F. ) ;
#9652=CARTESIAN_POINT ( 'NONE',  ( 25.63948732994507651, 45.16218137147968292, 74.70433879953100131 ) ) ;
#9654=CARTESIAN_POINT ( 'NONE',  ( 28.43948732994508077, 43.16218137147969003, 76.90433879953101837 ) ) ;
#9677=DIRECTION ( 'NONE',  ( 1.000000000000000000, 0.000000000000000000, 0.000000000000000000 ) ) ;
#9687=EDGE_CURVE ( 'NONE', #4876, #15492, #3101, .T. ) ;
#9725=CARTESIAN_POINT ( 'NONE',  ( 28.43948732994508077, 36.35905713404685713, 76.90433879953101837 ) ) ;
#9744=VECTOR ( 'NONE', #1399, 1000.000000000000000 ) ;
#9758=CARTESIAN_POINT ( 'NONE',  ( 27.63948732994508717, 45.16218137147969003, 74.70433879953098710 ) ) ;
#9768=LINE ( 'NONE', #8270, #14255 ) ;
#9780=VERTEX_POINT ( 'NONE', #3828 ) ;
#9799=LINE ( 'NONE', #16075, #16679 ) ;
#9805=ORIENTED_EDGE ( 'NONE', *, *, #13480, .F. ) ;
#9814=AXIS2_PLACEMENT_3D ( 'NONE', #18782, #13878, #20360 ) ;
#9847=VECTOR ( 'NONE', #11973, 1000.000000000000000 ) ;
#9861=VECTOR ( 'NONE', #12625, 1000.000000000000000 ) ;
#9862=CARTESIAN_POINT ( 'NONE',  ( 23.63948732994508006, 43.16218137147968292, 76.90433879953101837 ) ) ;
#9882=AXIS2_PLACEMENT_3D ( 'NONE', #10993, #7777, #14058 ) ;
#9896=( GEOMETRIC_REPRESENTATION_CONTEXT ( 3 ) GLOBAL_UNCERTAINTY_ASSIGNED_CONTEXT ( ( #21012 ) ) GLOBAL_UNIT_ASSIGNED_CONTEXT ( ( #1255, #9459, #1574 ) ) REPRESENTATION_CONTEXT ( 'NONE', 'WORKASPACE' ) );
#9901=EDGE_CURVE ( 'NONE', #7818, #11295, #5951, .T. ) ;
#9949=ORIENTED_EDGE ( 'NONE', *, *, #15786, .T. ) ;
#9951=CARTESIAN_POINT ( 'NONE',  ( 23.63948732994508006, 36.35905713404685002, 76.90433879953101837 ) ) ;
#9993=LINE ( 'NONE', #10090, #14927 ) ;
#9995=CYLINDRICAL_SURFACE ( 'NONE', #2818, 0.5999999999999894307 ) ;
#10017=CARTESIAN_POINT ( 'NONE',  ( 25.63948732994507651, 43.16218137147969003, 74.70433879953100131 ) ) ;
#10053=DIRECTION ( 'NONE',  ( -1.402518428993830937E-16, 1.000000000000000000, -3.469446951953617147E-16 ) ) ;
#10062=EDGE_CURVE ( 'NONE', #2511, #11695, #15172, .T. ) ;
#10070=ORIENTED_EDGE ( 'NONE', *, *, #6772, .F. ) ;
#10090=CARTESIAN_POINT ( 'NONE',  ( 31.03948732994507864, 36.35905713404685002, 78.30433879953099563 ) ) ;
#10114=DIRECTION ( 'NONE',  ( -1.402518428993830937E-16, 1.000000000000000000, -3.469446951953617147E-16 ) ) ;
#10122=ORIENTED_EDGE ( 'NONE', *, *, #10682, .F. ) ;
#10131=CARTESIAN_POINT ( 'NONE',  ( 30.43948732994507722, 45.16218137147968292, 74.70433879953098710 ) ) ;
#10138=EDGE_CURVE ( 'NONE', #6648, #20749, #17549, .T. ) ;
#10146=DIRECTION ( 'NONE',  ( -1.402518428993830937E-16, 1.000000000000000000, -3.469446951953617147E-16 ) ) ;
#10148=ADVANCED_FACE ( 'NONE', ( #504 ), #2428, .F. ) ;
#10157=ORIENTED_EDGE ( 'NONE', *, *, #16170, .T. ) ;
#10166=ORIENTED_EDGE ( 'NONE', *, *, #9901, .F. ) ;
#10189=ADVANCED_FACE ( 'NONE', ( #14021 ), #4114, .F. ) ;
#10208=CLOSED_SHELL ( 'NONE', ( #3508, #19874, #10189, #17792, #7646, #3642, #20423, #13505, #4029, #18308, #95, #151, #19867, #10148, #4765, #18160, #12508, #770, #20448, #3492, #8074, #5710, #3725, #3611, #20053, #16542, #76, #15573, #16228, #11031, #9632 ) ) ;
#10216=CIRCLE ( 'NONE', #1027, 0.5999999999999998668 ) ;
#10278=CARTESIAN_POINT ( 'NONE',  ( 23.03948732994508575, 43.16218137147968292, 76.90433879953101837 ) ) ;
#10298=DIRECTION ( 'NONE',  ( 1.000000000000000000, 0.000000000000000000, 0.000000000000000000 ) ) ;
#10322=VECTOR ( 'NONE', #18414, 1000.000000000000000 ) ;
#10343=CARTESIAN_POINT ( 'NONE',  ( 28.43948732994508077, 45.16218137147969003, 76.90433879953101837 ) ) ;
#10355=CIRCLE ( 'NONE', #2174, 1.399999999999995026 ) ;
#10365=ORIENTED_EDGE ( 'NONE', *, *, #7274, .T. ) ;
#10390=DIRECTION ( 'NONE',  ( 1.000000000000000000, 1.402518428993831183E-16, -4.344610079045915326E-32 ) ) ;
#10427=DIRECTION ( 'NONE',  ( 1.000000000000000000, 0.000000000000000000, 0.000000000000000000 ) ) ;
#10430=DIRECTION ( 'NONE',  ( 0.000000000000000000, 0.000000000000000000, 1.000000000000000000 ) ) ;
#10459=VECTOR ( 'NONE', #10053, 1000.000000000000000 ) ;
#10489=VECTOR ( 'NONE', #5768, 1000.000000000000000 ) ;
#10496=CARTESIAN_POINT ( 'NONE',  ( 23.03948732994508930, 27.61837231449496599, 76.90433879953101837 ) ) ;
#10525=FACE_OUTER_BOUND ( 'NONE', #19094, .T. ) ;
#10535=CARTESIAN_POINT ( 'NONE',  ( 29.03948732994507864, 36.35905713404685002, 74.70433879953100131 ) ) ;
#10616=CARTESIAN_POINT ( 'NONE',  ( 27.03948732994508930, 36.35905713404685713, 78.30433879953100984 ) ) ;
#10617=ORIENTED_EDGE ( 'NONE', *, *, #12741, .T. ) ;
#10659=DIRECTION ( 'NONE',  ( -1.402518428993831676E-16, 1.000000000000000000, -0.000000000000000000 ) ) ;
#10682=EDGE_CURVE ( 'NONE', #10795, #8152, #5565, .T. ) ;
#10703=EDGE_CURVE ( 'NONE', #6648, #7726, #241, .T. ) ;
#10708=LINE ( 'NONE', #18967, #464 ) ;
#10716=FACE_OUTER_BOUND ( 'NONE', #13681, .T. ) ;
#10719=ORIENTED_EDGE ( 'NONE', *, *, #6772, .T. ) ;
#10759=CARTESIAN_POINT ( 'NONE',  ( 31.03948732994507864, 43.16218137147969003, 78.30433879953099563 ) ) ;
#10766=ORIENTED_EDGE ( 'NONE', *, *, #4563, .F. ) ;
#10771=CARTESIAN_POINT ( 'NONE',  ( 23.03948732994508930, 27.61837231449496599, 78.60433879953100700 ) ) ;
#10773=CARTESIAN_POINT ( 'NONE',  ( 13.13948732994506230, 27.61837231449496244, 78.60433879953100700 ) ) ;
#10795=VERTEX_POINT ( 'NONE', #7263 ) ;
#10828=CARTESIAN_POINT ( 'NONE',  ( 23.03948732994508575, 36.35905713404685002, 76.90433879953101837 ) ) ;
#10846=ORIENTED_EDGE ( 'NONE', *, *, #11977, .F. ) ;
#10874=LINE ( 'NONE', #10771, #17244 ) ;
#10877=CYLINDRICAL_SURFACE ( 'NONE', #6048, 1.399999999999998579 ) ;
#10893=CIRCLE ( 'NONE', #13585, 0.5999999999999928724 ) ;
#10902=AXIS2_PLACEMENT_3D ( 'NONE', #4300, #19294, #218 ) ;
#10932=LINE ( 'NONE', #2828, #20387 ) ;
#10971=VERTEX_POINT ( 'NONE', #15880 ) ;
#10993=CARTESIAN_POINT ( 'NONE',  ( 27.03948732994508930, 36.35905713404685713, 76.90433879953101837 ) ) ;
#11014=AXIS2_PLACEMENT_3D ( 'NONE', #2904, #2690, #14385 ) ;
#11031=ADVANCED_FACE ( 'NONE', ( #6700 ), #13204, .T. ) ;
#11079=CARTESIAN_POINT ( 'NONE',  ( 23.03948732994508575, 45.16218137147969003, 76.90433879953101837 ) ) ;
#11087=PLANE ( 'NONE',  #9555 ) ;
#11091=CYLINDRICAL_SURFACE ( 'NONE', #9882, 1.399999999999998579 ) ;
#11173=EDGE_CURVE ( 'NONE', #2743, #1145, #15224, .T. ) ;
#11208=CARTESIAN_POINT ( 'NONE',  ( 24.43948732994508077, 36.35905713404685002, 76.90433879953101837 ) ) ;
#11219=VECTOR ( 'NONE', #18388, 1000.000000000000000 ) ;
#11236=AXIS2_PLACEMENT_3D ( 'NONE', #19609, #19298, #5032 ) ;
#11255=VERTEX_POINT ( 'NONE', #3930 ) ;
#11295=VERTEX_POINT ( 'NONE', #6259 ) ;
#11322=DIRECTION ( 'NONE',  ( -1.000000000000000000, -1.402518428993809243E-16, 6.308085367188358095E-15 ) ) ;
#11330=VECTOR ( 'NONE', #43, 1000.000000000000000 ) ;
#11352=ORIENTED_EDGE ( 'NONE', *, *, #8, .T. ) ;
#11390=DIRECTION ( 'NONE',  ( 1.000000000000000000, 0.000000000000000000, 0.000000000000000000 ) ) ;
#11396=CARTESIAN_POINT ( 'NONE',  ( 29.63948732994508006, 43.16218137147969003, 76.90433879953101837 ) ) ;
#11414=ORIENTED_EDGE ( 'NONE', *, *, #14856, .T. ) ;
#11426=DIRECTION ( 'NONE',  ( -1.402518428993831183E-16, 1.000000000000000000, -3.469446951953617640E-16 ) ) ;
#11428=ORIENTED_EDGE ( 'NONE', *, *, #16653, .F. ) ;
#11451=ORIENTED_EDGE ( 'NONE', *, *, #5810, .F. ) ;
#11544=DIRECTION ( 'NONE',  ( -0.7071067811865506814, 0.7071067811865443531, -2.453269466693389746E-16 ) ) ;
#11577=CARTESIAN_POINT ( 'NONE',  ( 30.43948732994507722, 43.16218137147969003, 74.70433879953098710 ) ) ;
#11602=CARTESIAN_POINT ( 'NONE',  ( 19.23948732994504240, 27.61837231449496599, 84.70433879953101552 ) ) ;
#11653=AXIS2_PLACEMENT_3D ( 'NONE', #11079, #19147, #11390 ) ;
#11671=MANIFOLD_SOLID_BREP ( 'Stock-MAS-160-1', #10208 ) ;
#11687=DIRECTION ( 'NONE',  ( 1.000000000000000000, 0.000000000000000000, 0.000000000000000000 ) ) ;
#11693=LINE ( 'NONE', #16575, #8202 ) ;
#11695=VERTEX_POINT ( 'NONE', #6339 ) ;
#11707=DIRECTION ( 'NONE',  ( 1.000000000000000000, 1.402518428993842277E-16, 3.154042683594179442E-15 ) ) ;
#11753=CARTESIAN_POINT ( 'NONE',  ( 25.85428507725097802, 26.43317006180084761, 75.00433879953101268 ) ) ;
#11770=EDGE_LOOP ( 'NONE', ( #15624, #15018, #19276, #5269 ) ) ;
#11803=FACE_OUTER_BOUND ( 'NONE', #12661, .T. ) ;
#11811=EDGE_CURVE ( 'NONE', #18002, #4756, #8371, .T. ) ;
#11816=CARTESIAN_POINT ( 'NONE',  ( 29.03948732994507864, 45.16218137147969003, 74.70433879953100131 ) ) ;
#11825=VERTEX_POINT ( 'NONE', #2044 ) ;
#11873=CARTESIAN_POINT ( 'NONE',  ( 23.63948732994508717, 45.16218137147969003, 74.70433879953098710 ) ) ;
#11914=PLANE ( 'NONE',  #7802 ) ;
#11921=ORIENTED_EDGE ( 'NONE', *, *, #17153, .T. ) ;
#11971=AXIS2_PLACEMENT_3D ( 'NONE', #7755, #1374, #1061 ) ;
#11973=DIRECTION ( 'NONE',  ( -1.000000000000000000, -1.402518428993831183E-16, 7.152522014899634076E-33 ) ) ;
#11977=EDGE_CURVE ( 'NONE', #3866, #19468, #2153, .T. ) ;
#11999=SHAPE_DEFINITION_REPRESENTATION ( #15161, #7678 ) ;
#12009=DIRECTION ( 'NONE',  ( 6.308085367188358884E-15, 3.469446951953626515E-16, 1.000000000000000000 ) ) ;
#12033=DIRECTION ( 'NONE',  ( -1.402518428993830937E-16, 1.000000000000000000, -3.469446951953617147E-16 ) ) ;
#12067=CARTESIAN_POINT ( 'NONE',  ( 23.03948732994508575, 36.35905713404685002, 77.50433879953099847 ) ) ;
#12113=CARTESIAN_POINT ( 'NONE',  ( 31.03948732994507864, 45.16218137147969003, 76.90433879953100416 ) ) ;
#12205=EDGE_LOOP ( 'NONE', ( #10766, #19310, #8356, #14833 ) ) ;
#12215=DIRECTION ( 'NONE',  ( -1.402518428993830937E-16, 1.000000000000000000, -3.469446951953617147E-16 ) ) ;
#12244=ORIENTED_EDGE ( 'NONE', *, *, #768, .T. ) ;
#12328=LINE ( 'NONE', #5608, #9169 ) ;
#12340=CIRCLE ( 'NONE', #11653, 0.5999999999999928724 ) ;
#12367=DIRECTION ( 'NONE',  ( -1.402518428993831676E-16, 1.000000000000000000, -0.000000000000000000 ) ) ;
#12379=FACE_OUTER_BOUND ( 'NONE', #19039, .T. ) ;
#12397=PLANE ( 'NONE',  #4418 ) ;
#12450=CARTESIAN_POINT ( 'NONE',  ( 29.63948732994508006, 36.35905713404685002, 76.90433879953101837 ) ) ;
#12479=ORIENTED_EDGE ( 'NONE', *, *, #901, .F. ) ;
#12483=FACE_OUTER_BOUND ( 'NONE', #15122, .T. ) ;
#12492=ORIENTED_EDGE ( 'NONE', *, *, #11173, .T. ) ;
#12500=EDGE_CURVE ( 'NONE', #14257, #5774, #11693, .T. ) ;
#12507=FACE_OUTER_BOUND ( 'NONE', #2508, .T. ) ;
#12508=ADVANCED_FACE ( 'NONE', ( #8171 ), #9995, .F. ) ;
#12533=PLANE ( 'NONE',  #328 ) ;
#12536=LINE ( 'NONE', #19022, #3992 ) ;
#12539=DIRECTION ( 'NONE',  ( 1.000000000000000000, 0.000000000000000000, 0.000000000000000000 ) ) ;
#12625=DIRECTION ( 'NONE',  ( 6.308085367188358884E-15, 3.469446951953626515E-16, 1.000000000000000000 ) ) ;
#12647=DIRECTION ( 'NONE',  ( 0.000000000000000000, 0.000000000000000000, 1.000000000000000000 ) ) ;
#12654=CARTESIAN_POINT ( 'NONE',  ( 27.03948732994508930, 45.16218137147969003, 76.90433879953101837 ) ) ;
#12661=EDGE_LOOP ( 'NONE', ( #4691, #14237, #12492, #8287 ) ) ;
#12687=ORIENTED_EDGE ( 'NONE', *, *, #2039, .T. ) ;
#12695=LINE ( 'NONE', #6393, #1778 ) ;
#12715=CYLINDRICAL_SURFACE ( 'NONE', #10902, 0.5999999999999894307 ) ;
#12741=EDGE_CURVE ( 'NONE', #10971, #6648, #2786, .T. ) ;
#12744=SURFACE_STYLE_FILL_AREA ( #17528 ) ;
#12759=DIRECTION ( 'NONE',  ( -1.402518428993831183E-16, 1.000000000000000000, -3.469446951953617640E-16 ) ) ;
#12803=EDGE_CURVE ( 'NONE', #18002, #13369, #17610, .T. ) ;
#12829=VERTEX_POINT ( 'NONE', #9654 ) ;
#12839=EDGE_CURVE ( 'NONE', #11295, #14257, #19749, .T. ) ;
#12890=ORIENTED_EDGE ( 'NONE', *, *, #12741, .F. ) ;
#12896=LINE ( 'NONE', #11208, #14064 ) ;
#12897=DIRECTION ( 'NONE',  ( 1.000000000000000000, 1.402518428993842277E-16, 3.154042683594179442E-15 ) ) ;
#12904=PLANE ( 'NONE',  #17341 ) ;
#12981=CIRCLE ( 'NONE', #14676, 0.5999999999999928724 ) ;
#13035=EDGE_CURVE ( 'NONE', #12829, #3770, #5012, .T. ) ;
#13036=PLANE ( 'NONE',  #11236 ) ;
#13057=LINE ( 'NONE', #272, #14603 ) ;
#13072=DIRECTION ( 'NONE',  ( 0.000000000000000000, -3.469446951953617640E-16, -1.000000000000000000 ) ) ;
#13089=DIRECTION ( 'NONE',  ( 1.402518428993831676E-16, -1.000000000000000000, 0.000000000000000000 ) ) ;
#13103=ORIENTED_EDGE ( 'NONE', *, *, #17085, .F. ) ;
#13148=CARTESIAN_POINT ( 'NONE',  ( 27.03948732994508219, 43.16218137147969003, 78.60433879953099279 ) ) ;
#13204=CYLINDRICAL_SURFACE ( 'NONE', #2615, 1.000000000000014655 ) ;
#13208=CARTESIAN_POINT ( 'NONE',  ( 27.63948732994508006, 36.35905713404685713, 76.90433879953101837 ) ) ;
#13210=DIRECTION ( 'NONE',  ( 1.734723475976781654E-15, -1.000000000000000000, 0.000000000000000000 ) ) ;
#13320=LINE ( 'NONE', #7016, #7148 ) ;
#13339=ORIENTED_EDGE ( 'NONE', *, *, #8590, .T. ) ;
#13369=VERTEX_POINT ( 'NONE', #19719 ) ;
#13371=DIRECTION ( 'NONE',  ( -1.000000000000000000, -1.402518428993831676E-16, 7.152522014899655971E-33 ) ) ;
#13391=EDGE_LOOP ( 'NONE', ( #15147, #6777, #19533, #11451 ) ) ;
#13423=CARTESIAN_POINT ( 'NONE',  ( 9.539487329945091076, 44.16218137147969713, 75.00433879953099847 ) ) ;
#13476=LINE ( 'NONE', #394, #16290 ) ;
#13477=CARTESIAN_POINT ( 'NONE',  ( 25.03948732994508219, 36.35905713404684292, 74.70433879953100131 ) ) ;
#13480=EDGE_CURVE ( 'NONE', #9281, #8992, #12695, .T. ) ;
#13482=CARTESIAN_POINT ( 'NONE',  ( 27.03948732994508219, 27.61837231449496599, 75.00433879953101268 ) ) ;
#13483=VERTEX_POINT ( 'NONE', #17791 ) ;
#13499=DIRECTION ( 'NONE',  ( -1.402518428993831676E-16, 1.000000000000000000, -0.000000000000000000 ) ) ;
#13505=ADVANCED_FACE ( 'NONE', ( #23 ), #20959, .T. ) ;
#13507=ORIENTED_EDGE ( 'NONE', *, *, #10138, .F. ) ;
#13559=ORIENTED_EDGE ( 'NONE', *, *, #2981, .F. ) ;
#13564=VECTOR ( 'NONE', #10146, 1000.000000000000000 ) ;
#13585=AXIS2_PLACEMENT_3D ( 'NONE', #14444, #4743, #9677 ) ;
#13625=CARTESIAN_POINT ( 'NONE',  ( 27.63948732994508006, 43.16218137147969003, 76.90433879953101837 ) ) ;
#13674=PLANE ( 'NONE',  #9814 ) ;
#13681=EDGE_LOOP ( 'NONE', ( #12479, #7477, #483, #9309 ) ) ;
#13797=EDGE_LOOP ( 'NONE', ( #4572, #7504, #18773, #18152 ) ) ;
#13805=DIRECTION ( 'NONE',  ( 5.731934358295347564E-32, -3.469446951953617147E-16, -1.000000000000000000 ) ) ;
#13830=DIRECTION ( 'NONE',  ( 3.154042683594179442E-15, -3.469446951953613203E-16, -1.000000000000000000 ) ) ;
#13860=LINE ( 'NONE', #18650, #16927 ) ;
#13878=DIRECTION ( 'NONE',  ( 1.000000000000000000, 1.402518428993842030E-16, 3.154042683594179047E-15 ) ) ;
#13886=DIRECTION ( 'NONE',  ( 6.308085367188358884E-15, 8.847205979147994320E-31, 1.000000000000000000 ) ) ;
#13893=EDGE_LOOP ( 'NONE', ( #17833, #548, #20996, #10846 ) ) ;
#13898=CARTESIAN_POINT ( 'NONE',  ( 27.03948732994508930, 43.16218137147969003, 76.90433879953101837 ) ) ;
#13905=ORIENTED_EDGE ( 'NONE', *, *, #14455, .T. ) ;
#13929=CARTESIAN_POINT ( 'NONE',  ( 23.03948732994508575, 45.16218137147969003, 76.90433879953101837 ) ) ;
#14021=FACE_OUTER_BOUND ( 'NONE', #17087, .T. ) ;
#14058=DIRECTION ( 'NONE',  ( 0.000000000000000000, 0.000000000000000000, 1.000000000000000000 ) ) ;
#14064=VECTOR ( 'NONE', #1519, 1000.000000000000000 ) ;
#14081=VERTEX_POINT ( 'NONE', #18578 ) ;
#14133=DIRECTION ( 'NONE',  ( -1.402518428993831183E-16, 1.000000000000000000, -3.469446951953617640E-16 ) ) ;
#14203=CIRCLE ( 'NONE', #18960, 0.5999999999999928724 ) ;
#14215=CARTESIAN_POINT ( 'NONE',  ( 23.03948732994508930, 27.61837231449496244, 73.00433879953101268 ) ) ;
#14225=FILL_AREA_STYLE_COLOUR ( '', #7027 ) ;
#14237=ORIENTED_EDGE ( 'NONE', *, *, #6506, .T. ) ;
#14255=VECTOR ( 'NONE', #13371, 1000.000000000000000 ) ;
#14256=CIRCLE ( 'NONE', #4744, 1.399999999999995026 ) ;
#14257=VERTEX_POINT ( 'NONE', #5920 ) ;
#14260=ORIENTED_EDGE ( 'NONE', *, *, #20158, .T. ) ;
#14281=VECTOR ( 'NONE', #1775, 1000.000000000000000 ) ;
#14294=VERTEX_POINT ( 'NONE', #3146 ) ;
#14329=VECTOR ( 'NONE', #17224, 1000.000000000000000 ) ;
#14355=ORIENTED_EDGE ( 'NONE', *, *, #10703, .F. ) ;
#14362=DIRECTION ( 'NONE',  ( 5.731934358295347564E-32, -3.469446951953617147E-16, -1.000000000000000000 ) ) ;
#14385=DIRECTION ( 'NONE',  ( -1.402518428993831183E-16, 1.000000000000000000, 0.000000000000000000 ) ) ;
#14388=CARTESIAN_POINT ( 'NONE',  ( 28.43948732994508077, 36.35905713404685713, 76.90433879953101837 ) ) ;
#14390=ORIENTED_EDGE ( 'NONE', *, *, #5279, .F. ) ;
#14444=CARTESIAN_POINT ( 'NONE',  ( 27.03948732994508930, 45.16218137147969003, 76.90433879953101837 ) ) ;
#14455=EDGE_CURVE ( 'NONE', #3770, #15492, #7224, .T. ) ;
#14483=VERTEX_POINT ( 'NONE', #20196 ) ;
#14492=EDGE_LOOP ( 'NONE', ( #4481, #2372, #8262, #6958 ) ) ;
#14501=DIRECTION ( 'NONE',  ( -1.402518428993831183E-16, 1.000000000000000000, -3.469446951953617640E-16 ) ) ;
#14573=CARTESIAN_POINT ( 'NONE',  ( 27.03948732994508930, 45.16218137147969003, 77.50433879953099847 ) ) ;
#14603=VECTOR ( 'NONE', #19531, 1000.000000000000000 ) ;
#14614=AXIS2_PLACEMENT_3D ( 'NONE', #5915, #18573, #10298 ) ;
#14643=DIRECTION ( 'NONE',  ( -1.402518428993830937E-16, 1.000000000000000000, -3.469446951953617147E-16 ) ) ;
#14676=AXIS2_PLACEMENT_3D ( 'NONE', #6881, #5379, #8492 ) ;
#14706=EDGE_LOOP ( 'NONE', ( #15055, #17870, #11921, #5093 ) ) ;
#14709=ORIENTED_EDGE ( 'NONE', *, *, #4301, .F. ) ;
#14761=EDGE_LOOP ( 'NONE', ( #13507, #8533, #1393, #8978 ) ) ;
#14783=CARTESIAN_POINT ( 'NONE',  ( 28.43948732994508788, 43.16218137147969003, 74.70433879953100131 ) ) ;
#14790=EDGE_CURVE ( 'NONE', #5251, #18002, #20472, .T. ) ;
#14811=ORIENTED_EDGE ( 'NONE', *, *, #19884, .F. ) ;
#14819=LINE ( 'NONE', #16321, #4127 ) ;
#14833=ORIENTED_EDGE ( 'NONE', *, *, #2302, .F. ) ;
#14838=CYLINDRICAL_SURFACE ( 'NONE', #1028, 0.5999999999999894307 ) ;
#14850=FACE_OUTER_BOUND ( 'NONE', #4903, .T. ) ;
#14854=DIRECTION ( 'NONE',  ( 6.308085367188358884E-15, 8.847205979147994320E-31, 1.000000000000000000 ) ) ;
#14856=EDGE_CURVE ( 'NONE', #9071, #3866, #4393, .T. ) ;
#14866=CARTESIAN_POINT ( 'NONE',  ( 26.43948732994507367, 43.16218137147969003, 74.70433879953098710 ) ) ;
#14890=ORIENTED_EDGE ( 'NONE', *, *, #520, .F. ) ;
#14898=DIRECTION ( 'NONE',  ( 3.154042683594179442E-15, 4.423602989573997160E-31, -1.000000000000000000 ) ) ;
#14905=CARTESIAN_POINT ( 'NONE',  ( 23.03948732994508575, 45.16218137147969003, 76.90433879953100416 ) ) ;
#14912=LINE ( 'NONE', #19590, #13564 ) ;
#14927=VECTOR ( 'NONE', #6879, 1000.000000000000000 ) ;
#14948=DIRECTION ( 'NONE',  ( 1.000000000000000000, 1.402518428993831676E-16, 1.213361030872719641E-32 ) ) ;
#14950=ORIENTED_EDGE ( 'NONE', *, *, #12839, .F. ) ;
#14984=ORIENTED_EDGE ( 'NONE', *, *, #11811, .F. ) ;
#14998=AXIS2_PLACEMENT_3D ( 'NONE', #19251, #1390, #4664 ) ;
#15018=ORIENTED_EDGE ( 'NONE', *, *, #5720, .T. ) ;
#15055=ORIENTED_EDGE ( 'NONE', *, *, #2596, .F. ) ;
#15057=DIRECTION ( 'NONE',  ( 0.000000000000000000, 0.000000000000000000, 1.000000000000000000 ) ) ;
#15086=ORIENTED_EDGE ( 'NONE', *, *, #16653, .T. ) ;
#15100=CARTESIAN_POINT ( 'NONE',  ( 27.63948732994508006, 36.35905713404685713, 76.90433879953101837 ) ) ;
#15105=EDGE_CURVE ( 'NONE', #7082, #3641, #20816, .T. ) ;
#15122=EDGE_LOOP ( 'NONE', ( #15538, #2393, #18911, #3629 ) ) ;
#15134=DIRECTION ( 'NONE',  ( 1.000000000000000000, 1.402518428993831183E-16, 1.213361030872721283E-32 ) ) ;
#15136=CARTESIAN_POINT ( 'NONE',  ( 24.43948732994508077, 45.16218137147969003, 76.90433879953101837 ) ) ;
#15147=ORIENTED_EDGE ( 'NONE', *, *, #17153, .F. ) ;
#15154=ORIENTED_EDGE ( 'NONE', *, *, #7235, .F. ) ;
#15161=PRODUCT_DEFINITION_SHAPE ( 'NONE', 'NONE',  #8857 ) ;
#15172=CIRCLE ( 'NONE', #16192, 0.5999999999999928724 ) ;
#15211=CARTESIAN_POINT ( 'NONE',  ( 24.43948732994508788, 45.16218137147969003, 74.70433879953100131 ) ) ;
#15224=LINE ( 'NONE', #5534, #6349 ) ;
#15243=ORIENTED_EDGE ( 'NONE', *, *, #14856, .F. ) ;
#15245=AXIS2_PLACEMENT_3D ( 'NONE', #17265, #16949, #4177 ) ;
#15293=AXIS2_PLACEMENT_3D ( 'NONE', #10828, #15709, #16016 ) ;
#15306=DIRECTION ( 'NONE',  ( 1.000000000000000000, 1.402518428993831183E-16, -4.865963288531423895E-32 ) ) ;
#15419=DIRECTION ( 'NONE',  ( -1.402518428993831183E-16, 1.000000000000000000, -3.469446951953617640E-16 ) ) ;
#15480=DIRECTION ( 'NONE',  ( -1.000000000000000000, -1.402518428993809490E-16, 6.308085367188358884E-15 ) ) ;
#15492=VERTEX_POINT ( 'NONE', #18071 ) ;
#15497=LINE ( 'NONE', #908, #6103 ) ;
#15528=AXIS2_PLACEMENT_3D ( 'NONE', #12113, #2316, #15306 ) ;
#15538=ORIENTED_EDGE ( 'NONE', *, *, #4025, .T. ) ;
#15573=ADVANCED_FACE ( 'NONE', ( #10525 ), #7310, .T. ) ;
#15583=DIRECTION ( 'NONE',  ( 0.000000000000000000, 0.000000000000000000, 1.000000000000000000 ) ) ;
#15613=DIRECTION ( 'NONE',  ( 1.000000000000000000, 0.000000000000000000, 0.000000000000000000 ) ) ;
#15624=ORIENTED_EDGE ( 'NONE', *, *, #14790, .F. ) ;
#15692=AXIS2_PLACEMENT_3D ( 'NONE', #224, #330, #4900 ) ;
#15709=DIRECTION ( 'NONE',  ( -1.402518428993830937E-16, 1.000000000000000000, -3.469446951953617147E-16 ) ) ;
#15766=DIRECTION ( 'NONE',  ( -1.402518428993831183E-16, 1.000000000000000000, -3.469446951953617147E-16 ) ) ;
#15786=EDGE_CURVE ( 'NONE', #4554, #14081, #19990, .T. ) ;
#15792=CARTESIAN_POINT ( 'NONE',  ( 25.03948732994508219, 43.16218137147969003, 74.70433879953100131 ) ) ;
#15837=VERTEX_POINT ( 'NONE', #20976 ) ;
#15880=CARTESIAN_POINT ( 'NONE',  ( 26.43948732994508788, 43.16218137147969003, 76.90433879953101837 ) ) ;
#15884=EDGE_LOOP ( 'NONE', ( #14355, #12890, #18502, #12687 ) ) ;
#15911=ORIENTED_EDGE ( 'NONE', *, *, #2635, .F. ) ;
#15943=SHAPE_REPRESENTATION_RELATIONSHIP ( 'NONE' , 'NONE' ,  #7678, #9085 ) ;
#15952=PLANE ( 'NONE',  #11971 ) ;
#15958=EDGE_CURVE ( 'NONE', #20749, #5251, #5856, .T. ) ;
#15972=FACE_OUTER_BOUND ( 'NONE', #16986, .T. ) ;
#15989=DIRECTION ( 'NONE',  ( 1.000000000000000000, 0.000000000000000000, 0.000000000000000000 ) ) ;
#16003=ORIENTED_EDGE ( 'NONE', *, *, #1080, .F. ) ;
#16016=DIRECTION ( 'NONE',  ( 0.000000000000000000, 0.000000000000000000, 1.000000000000000000 ) ) ;
#16030=CARTESIAN_POINT ( 'NONE',  ( 29.63948732994508006, 45.16218137147968292, 74.70433879953100131 ) ) ;
#16038=DIRECTION ( 'NONE',  ( -1.402518428993831183E-16, 1.000000000000000000, -3.469446951953617147E-16 ) ) ;
#16075=CARTESIAN_POINT ( 'NONE',  ( 25.63948732994508362, 36.35905713404684292, 76.90433879953101837 ) ) ;
#16103=AXIS2_PLACEMENT_3D ( 'NONE', #4854, #19325, #12539 ) ;
#16135=DIRECTION ( 'NONE',  ( 6.308085367188358884E-15, 3.469446951953626515E-16, 1.000000000000000000 ) ) ;
#16137=CARTESIAN_POINT ( 'NONE',  ( 31.03948732994507864, 45.16218137147969003, 76.90433879953100416 ) ) ;
#16153=CARTESIAN_POINT ( 'NONE',  ( 0.000000000000000000, 0.000000000000000000, 0.000000000000000000 ) ) ;
#16170=EDGE_CURVE ( 'NONE', #16996, #5038, #1380, .T. ) ;
#16191=CARTESIAN_POINT ( 'NONE',  ( 26.43948732994507367, 45.16218137147968292, 74.70433879953098710 ) ) ;
#16192=AXIS2_PLACEMENT_3D ( 'NONE', #8613, #5506, #18274 ) ;
#16215=ORIENTED_EDGE ( 'NONE', *, *, #12500, .T. ) ;
#16228=ADVANCED_FACE ( 'NONE', ( #4975 ), #17861, .T. ) ;
#16252=( LENGTH_UNIT ( ) NAMED_UNIT ( * ) SI_UNIT ( .MILLI., .METRE. ) );
#16290=VECTOR ( 'NONE', #12009, 1000.000000000000000 ) ;
#16321=CARTESIAN_POINT ( 'NONE',  ( 23.03948732994508575, 45.16218137147969003, 76.90433879953100416 ) ) ;
#16345=LINE ( 'NONE', #20803, #14281 ) ;
#16353=CARTESIAN_POINT ( 'NONE',  ( 25.03948732994508219, 36.35905713404684292, 74.70433879953100131 ) ) ;
#16368=VECTOR ( 'NONE', #15134, 1000.000000000000000 ) ;
#16419=ORIENTED_EDGE ( 'NONE', *, *, #20414, .F. ) ;
#16475=ORIENTED_EDGE ( 'NONE', *, *, #7153, .F. ) ;
#16511=ORIENTED_EDGE ( 'NONE', *, *, #3228, .T. ) ;
#16532=DIRECTION ( 'NONE',  ( -1.402518428993831183E-16, 1.000000000000000000, -3.469446951953617640E-16 ) ) ;
#16542=ADVANCED_FACE ( 'NONE', ( #12483 ), #7594, .T. ) ;
#16558=DIRECTION ( 'NONE',  ( 0.000000000000000000, 0.000000000000000000, 1.000000000000000000 ) ) ;
#16575=CARTESIAN_POINT ( 'NONE',  ( 31.03948732994507864, 45.16218137147969003, 78.30433879953099563 ) ) ;
#16603=DIRECTION ( 'NONE',  ( 5.731934358295347564E-32, -3.469446951953617147E-16, -1.000000000000000000 ) ) ;
#16620=LINE ( 'NONE', #14905, #5482 ) ;
#16621=ORIENTED_EDGE ( 'NONE', *, *, #5323, .T. ) ;
#16653=EDGE_CURVE ( 'NONE', #4876, #14294, #4205, .T. ) ;
#16656=AXIS2_PLACEMENT_3D ( 'NONE', #13423, #752, #13210 ) ;
#16661=CARTESIAN_POINT ( 'NONE',  ( 8.832380548758539618, 43.45507459029313679, 75.00433879953099847 ) ) ;
#16679=VECTOR ( 'NONE', #1499, 1000.000000000000000 ) ;
#16710=DIRECTION ( 'NONE',  ( 3.154042683594179442E-15, -3.469446951953613203E-16, -1.000000000000000000 ) ) ;
#16738=LINE ( 'NONE', #7255, #10489 ) ;
#16740=VERTEX_POINT ( 'NONE', #17548 ) ;
#16743=ORIENTED_EDGE ( 'NONE', *, *, #9499, .T. ) ;
#16753=ORIENTED_EDGE ( 'NONE', *, *, #3034, .T. ) ;
#16800=FACE_OUTER_BOUND ( 'NONE', #20774, .T. ) ;
#16811=CARTESIAN_POINT ( 'NONE',  ( 23.03948732994508575, 43.16218137147969003, 78.60433879953099279 ) ) ;
#16824=CARTESIAN_POINT ( 'NONE',  ( 27.63948732994508006, 43.16218137147969003, 76.90433879953101837 ) ) ;
#16859=DIRECTION ( 'NONE',  ( -1.402518428993831183E-16, 1.000000000000000000, 0.000000000000000000 ) ) ;
#16881=ORIENTED_EDGE ( 'NONE', *, *, #7694, .T. ) ;
#16927=VECTOR ( 'NONE', #8768, 1000.000000000000000 ) ;
#16949=DIRECTION ( 'NONE',  ( -5.731934358295347564E-32, 3.469446951953617147E-16, 1.000000000000000000 ) ) ;
#16971=AXIS2_PLACEMENT_3D ( 'NONE', #4447, #10659, #17014 ) ;
#16986=EDGE_LOOP ( 'NONE', ( #8456, #8379, #5074, #21027 ) ) ;
#16996=VERTEX_POINT ( 'NONE', #5986 ) ;
#16998=CARTESIAN_POINT ( 'NONE',  ( 23.63948732994508006, 45.16218137147969003, 76.90433879953101837 ) ) ;
#16999=CARTESIAN_POINT ( 'NONE',  ( 27.03948732994508930, 43.16218137147969003, 76.90433879953101837 ) ) ;
#17009=EDGE_CURVE ( 'NONE', #5038, #1468, #10708, .T. ) ;
#17011=EDGE_LOOP ( 'NONE', ( #6484, #17188, #5254, #18777 ) ) ;
#17014=DIRECTION ( 'NONE',  ( 1.000000000000000000, 0.000000000000000000, 0.000000000000000000 ) ) ;
#17049=AXIS2_PLACEMENT_3D ( 'NONE', #1169, #14133, #4647 ) ;
#17085=EDGE_CURVE ( 'NONE', #8173, #6536, #10355, .T. ) ;
#17087=EDGE_LOOP ( 'NONE', ( #19370, #12244, #5685, #16475 ) ) ;
#17153=EDGE_CURVE ( 'NONE', #9281, #3928, #12896, .T. ) ;
#17169=DIRECTION ( 'NONE',  ( 0.7071067811865460184, 9.917302918806395333E-17, 0.7071067811865490160 ) ) ;
#17188=ORIENTED_EDGE ( 'NONE', *, *, #17818, .T. ) ;
#17204=ORIENTED_EDGE ( 'NONE', *, *, #18296, .F. ) ;
#17217=DIRECTION ( 'NONE',  ( -1.402518428993831183E-16, 1.000000000000000000, -3.469446951953617640E-16 ) ) ;
#17224=DIRECTION ( 'NONE',  ( -4.865963288531424442E-32, -6.824603186972751860E-48, -1.000000000000000000 ) ) ;
#17235=LINE ( 'NONE', #17347, #6707 ) ;
#17244=VECTOR ( 'NONE', #15766, 1000.000000000000000 ) ;
#17265=CARTESIAN_POINT ( 'NONE',  ( 9.539487329945091076, 44.16218137147969713, 73.00433879953099847 ) ) ;
#17323=CYLINDRICAL_SURFACE ( 'NONE', #4161, 1.399999999999998579 ) ;
#17341=AXIS2_PLACEMENT_3D ( 'NONE', #4803, #11322, #5995 ) ;
#17347=CARTESIAN_POINT ( 'NONE',  ( 8.832380548758539618, 43.45507459029314390, 95.45352954694192249 ) ) ;
#17350=DIRECTION ( 'NONE',  ( -1.402518428993831183E-16, 1.000000000000000000, -3.469446951953617640E-16 ) ) ;
#17388=CARTESIAN_POINT ( 'NONE',  ( 19.23948732994503885, 45.16218137147969003, 84.70433879953101552 ) ) ;
#17398=FACE_OUTER_BOUND ( 'NONE', #14706, .T. ) ;
#17399=AXIS2_PLACEMENT_3D ( 'NONE', #13929, #20410, #17438 ) ;
#17438=DIRECTION ( 'NONE',  ( 1.000000000000000000, 0.000000000000000000, 0.000000000000000000 ) ) ;
#17449=EDGE_CURVE ( 'NONE', #19468, #4403, #16620, .T. ) ;
#17493=EDGE_CURVE ( 'NONE', #7818, #9780, #19405, .T. ) ;
#17505=ORIENTED_EDGE ( 'NONE', *, *, #20258, .T. ) ;
#17510=EDGE_LOOP ( 'NONE', ( #1831, #8701, #14709, #6090, #14890, #18897, #13559, #13103, #3787, #19733, #9531, #16621, #14811, #11414, #633, #20576, #6823, #8990, #18267, #20275, #2555, #9024, #13905, #20471, #16511, #18258, #16215 ) ) ;
#17522=LINE ( 'NONE', #7847, #4333 ) ;
#17527=DIRECTION ( 'NONE',  ( -1.402518428993831183E-16, 1.000000000000000000, -3.469446951953617640E-16 ) ) ;
#17528=FILL_AREA_STYLE ('',( #14225 ) ) ;
#17534=CARTESIAN_POINT ( 'NONE',  ( 9.539487329945080418, 43.16218137147968292, 75.00433879953099847 ) ) ;
#17548=CARTESIAN_POINT ( 'NONE',  ( 26.43948732994508788, 45.16218137147969003, 76.90433879953101837 ) ) ;
#17549=CIRCLE ( 'NONE', #4282, 0.5999999999999928724 ) ;
#17562=ORIENTED_EDGE ( 'NONE', *, *, #7826, .T. ) ;
#17593=ORIENTED_EDGE ( 'NONE', *, *, #1080, .T. ) ;
#17605=ORIENTED_EDGE ( 'NONE', *, *, #10682, .T. ) ;
#17610=LINE ( 'NONE', #6322, #5494 ) ;
#17612=ORIENTED_EDGE ( 'NONE', *, *, #11811, .T. ) ;
#17623=ORIENTED_EDGE ( 'NONE', *, *, #18748, .F. ) ;
#17648=VECTOR ( 'NONE', #20715, 1000.000000000000000 ) ;
#17657=CARTESIAN_POINT ( 'NONE',  ( 27.03948732994508930, 43.16218137147969003, 76.90433879953101837 ) ) ;
#17685=DIRECTION ( 'NONE',  ( 3.154042683594179047E-15, 4.423602989573997160E-31, -1.000000000000000000 ) ) ;
#17738=DIRECTION ( 'NONE',  ( -6.079324319404144630E-32, 3.469446951953617147E-16, 1.000000000000000000 ) ) ;
#17745=ORIENTED_EDGE ( 'NONE', *, *, #18621, .F. ) ;
#17756=VECTOR ( 'NONE', #4290, 1000.000000000000114 ) ;
#17791=CARTESIAN_POINT ( 'NONE',  ( 23.03948732994508575, 43.16218137147969003, 73.00433879953099847 ) ) ;
#17792=ADVANCED_FACE ( 'NONE', ( #15972 ), #7774, .T. ) ;
#17818=EDGE_CURVE ( 'NONE', #4298, #12829, #2777, .T. ) ;
#17833=ORIENTED_EDGE ( 'NONE', *, *, #7694, .F. ) ;
#17861=PLANE ( 'NONE',  #18136 ) ;
#17870=ORIENTED_EDGE ( 'NONE', *, *, #5279, .T. ) ;
#17894=CARTESIAN_POINT ( 'NONE',  ( 23.03948732994508575, 36.35905713404685002, 78.30433879953099563 ) ) ;
#17917=LINE ( 'NONE', #6418, #18327 ) ;
#17953=EDGE_CURVE ( 'NONE', #4353, #11695, #2547, .T. ) ;
#17957=CARTESIAN_POINT ( 'NONE',  ( 9.539487329945082195, 27.61837231449496244, 75.00433879953101268 ) ) ;
#17962=ORIENTED_EDGE ( 'NONE', *, *, #8570, .F. ) ;
#18002=VERTEX_POINT ( 'NONE', #18608 ) ;
#18017=VECTOR ( 'NONE', #6273, 1000.000000000000000 ) ;
#18071=CARTESIAN_POINT ( 'NONE',  ( 28.43948732994508788, 45.16218137147969003, 74.70433879953100131 ) ) ;
#18136=AXIS2_PLACEMENT_3D ( 'NONE', #11602, #6679, #3285 ) ;
#18137=VERTEX_POINT ( 'NONE', #16811 ) ;
#18152=ORIENTED_EDGE ( 'NONE', *, *, #4784, .F. ) ;
#18160=ADVANCED_FACE ( 'NONE', ( #5842 ), #15952, .T. ) ;
#18215=CARTESIAN_POINT ( 'NONE',  ( 27.03948732994508930, 45.16218137147969003, 76.90433879953101837 ) ) ;
#18258=ORIENTED_EDGE ( 'NONE', *, *, #12839, .T. ) ;
#18267=ORIENTED_EDGE ( 'NONE', *, *, #10062, .T. ) ;
#18272=EDGE_CURVE ( 'NONE', #4403, #3928, #20441, .T. ) ;
#18274=DIRECTION ( 'NONE',  ( 1.000000000000000000, 0.000000000000000000, 0.000000000000000000 ) ) ;
#18283=ORIENTED_EDGE ( 'NONE', *, *, #9687, .F. ) ;
#18296=EDGE_CURVE ( 'NONE', #9780, #6140, #19231, .T. ) ;
#18308=ADVANCED_FACE ( 'NONE', ( #7545 ), #2960, .F. ) ;
#18322=VECTOR ( 'NONE', #5505, 1000.000000000000000 ) ;
#18327=VECTOR ( 'NONE', #1863, 1000.000000000000000 ) ;
#18366=AXIS2_PLACEMENT_3D ( 'NONE', #16153, #12647, #3061 ) ;
#18379=EDGE_LOOP ( 'NONE', ( #19738, #10365, #19412, #19012 ) ) ;
#18388=DIRECTION ( 'NONE',  ( -4.344610079045915326E-32, -6.093395702654244599E-48, -1.000000000000000000 ) ) ;
#18398=DIRECTION ( 'NONE',  ( 1.000000000000000000, 0.000000000000000000, 0.000000000000000000 ) ) ;
#18414=DIRECTION ( 'NONE',  ( 3.154042683594179442E-15, 4.423602989573997160E-31, -1.000000000000000000 ) ) ;
#18452=AXIS2_PLACEMENT_3D ( 'NONE', #13482, #4108, #8609 ) ;
#18502=ORIENTED_EDGE ( 'NONE', *, *, #2302, .T. ) ;
#18530=ORIENTED_EDGE ( 'NONE', *, *, #20533, .T. ) ;
#18532=ORIENTED_EDGE ( 'NONE', *, *, #19884, .T. ) ;
#18573=DIRECTION ( 'NONE',  ( -1.402518428993831676E-16, 1.000000000000000000, -0.000000000000000000 ) ) ;
#18578=CARTESIAN_POINT ( 'NONE',  ( 23.63948732994508006, 45.16218137147969003, 76.90433879953101837 ) ) ;
#18597=DIRECTION ( 'NONE',  ( -1.000000000000000000, -1.402518428993809490E-16, 6.308085367188358884E-15 ) ) ;
#18608=CARTESIAN_POINT ( 'NONE',  ( 30.43948732994507722, 43.16218137147969003, 74.70433879953098710 ) ) ;
#18617=VERTEX_POINT ( 'NONE', #14866 ) ;
#18621=EDGE_CURVE ( 'NONE', #15492, #3149, #12981, .T. ) ;
#18650=CARTESIAN_POINT ( 'NONE',  ( 25.63948732994507651, 43.16218137147969003, 74.70433879953100131 ) ) ;
#18685=AXIS2_PLACEMENT_3D ( 'NONE', #2406, #9010, #3780 ) ;
#18702=CARTESIAN_POINT ( 'NONE',  ( 31.03948732994507864, 36.35905713404685002, 76.90433879953100416 ) ) ;
#18748=EDGE_CURVE ( 'NONE', #8152, #11825, #14819, .T. ) ;
#18773=ORIENTED_EDGE ( 'NONE', *, *, #15105, .F. ) ;
#18777=ORIENTED_EDGE ( 'NONE', *, *, #3836, .F. ) ;
#18782=CARTESIAN_POINT ( 'NONE',  ( 23.63948732994508006, 36.35905713404685002, 76.90433879953101837 ) ) ;
#18843=DIRECTION ( 'NONE',  ( 1.000000000000000000, 0.000000000000000000, 0.000000000000000000 ) ) ;
#18885=LINE ( 'NONE', #10616, #7108 ) ;
#18897=ORIENTED_EDGE ( 'NONE', *, *, #2039, .F. ) ;
#18911=ORIENTED_EDGE ( 'NONE', *, *, #17449, .F. ) ;
#18960=AXIS2_PLACEMENT_3D ( 'NONE', #15792, #19268, #15989 ) ;
#18967=CARTESIAN_POINT ( 'NONE',  ( 19.23948732994504240, 43.16218137147968292, 84.70433879953101552 ) ) ;
#18991=CARTESIAN_POINT ( 'NONE',  ( 9.125273767571993488, 43.16218137147969003, 73.00433879953099847 ) ) ;
#19012=ORIENTED_EDGE ( 'NONE', *, *, #3277, .F. ) ;
#19017=AXIS2_PLACEMENT_3D ( 'NONE', #10278, #3452, #251 ) ;
#19020=CARTESIAN_POINT ( 'NONE',  ( 27.03948732994508219, 27.61837231449496599, 78.60433879953100700 ) ) ;
#19022=CARTESIAN_POINT ( 'NONE',  ( 31.03948732994507864, 36.35905713404685002, 77.50433879953099847 ) ) ;
#19032=VECTOR ( 'NONE', #5157, 1000.000000000000000 ) ;
#19039=EDGE_LOOP ( 'NONE', ( #715, #10719, #1777, #16003 ) ) ;
#19052=VECTOR ( 'NONE', #14948, 1000.000000000000000 ) ;
#19068=CARTESIAN_POINT ( 'NONE',  ( 8.832380548758539618, 43.45507459029314390, 95.45352954694192249 ) ) ;
#19074=ORIENTED_EDGE ( 'NONE', *, *, #8590, .F. ) ;
#19094=EDGE_LOOP ( 'NONE', ( #779, #20738, #15154, #10157 ) ) ;
#19097=AXIS2_PLACEMENT_3D ( 'NONE', #16137, #7628, #20591 ) ;
#19147=DIRECTION ( 'NONE',  ( -1.402518428993831183E-16, 1.000000000000000000, -3.469446951953617640E-16 ) ) ;
#19207=ORIENTED_EDGE ( 'NONE', *, *, #20265, .T. ) ;
#19231=LINE ( 'NONE', #10759, #14329 ) ;
#19251=CARTESIAN_POINT ( 'NONE',  ( 31.03948732994507864, 36.35905713404685002, 78.30433879953099563 ) ) ;
#19268=DIRECTION ( 'NONE',  ( 1.402518428993831676E-16, -1.000000000000000000, 0.000000000000000000 ) ) ;
#19276=ORIENTED_EDGE ( 'NONE', *, *, #4301, .T. ) ;
#19294=DIRECTION ( 'NONE',  ( -1.402518428993831183E-16, 1.000000000000000000, -3.469446951953617640E-16 ) ) ;
#19298=DIRECTION ( 'NONE',  ( 1.000000000000000000, 1.402518428993842030E-16, 3.154042683594179047E-15 ) ) ;
#19305=DIRECTION ( 'NONE',  ( -1.402518428993831183E-16, 1.000000000000000000, -3.469446951953617640E-16 ) ) ;
#19310=ORIENTED_EDGE ( 'NONE', *, *, #9304, .T. ) ;
#19325=DIRECTION ( 'NONE',  ( 1.402518428993831676E-16, -1.000000000000000000, 0.000000000000000000 ) ) ;
#19339=VECTOR ( 'NONE', #16603, 1000.000000000000000 ) ;
#19347=AXIS2_PLACEMENT_3D ( 'NONE', #516, #13499, #18398 ) ;
#19370=ORIENTED_EDGE ( 'NONE', *, *, #2813, .F. ) ;
#19405=CIRCLE ( 'NONE', #15692, 1.399999999999995026 ) ;
#19412=ORIENTED_EDGE ( 'NONE', *, *, #4784, .T. ) ;
#19468=VERTEX_POINT ( 'NONE', #2660 ) ;
#19476=DIRECTION ( 'NONE',  ( -1.402518428993831183E-16, 1.000000000000000000, -3.469446951953617640E-16 ) ) ;
#19531=DIRECTION ( 'NONE',  ( -1.402518428993831183E-16, 1.000000000000000000, -3.469446951953617640E-16 ) ) ;
#19533=ORIENTED_EDGE ( 'NONE', *, *, #5592, .T. ) ;
#19590=CARTESIAN_POINT ( 'NONE',  ( 26.43948732994508788, 36.35905713404684292, 76.90433879953101837 ) ) ;
#19609=CARTESIAN_POINT ( 'NONE',  ( 24.43948732994508077, 36.35905713404685002, 76.90433879953101837 ) ) ;
#19632=DIRECTION ( 'NONE',  ( -1.402518428993830937E-16, 1.000000000000000000, -3.469446951953617147E-16 ) ) ;
#19635=( NAMED_UNIT ( * ) SI_UNIT ( $, .STERADIAN. ) SOLID_ANGLE_UNIT ( ) );
#19641=EDGE_CURVE ( 'NONE', #8152, #14081, #12340, .T. ) ;
#19692=CIRCLE ( 'NONE', #16656, 1.000000000000014655 ) ;
#19719=CARTESIAN_POINT ( 'NONE',  ( 30.43948732994507722, 45.16218137147968292, 74.70433879953098710 ) ) ;
#19733=ORIENTED_EDGE ( 'NONE', *, *, #19641, .F. ) ;
#19738=ORIENTED_EDGE ( 'NONE', *, *, #17953, .F. ) ;
#19749=CIRCLE ( 'NONE', #19097, 1.399999999999995026 ) ;
#19852=ORIENTED_EDGE ( 'NONE', *, *, #20704, .T. ) ;
#19854=DIRECTION ( 'NONE',  ( -1.402518428993830937E-16, 1.000000000000000000, -3.469446951953617147E-16 ) ) ;
#19867=ADVANCED_FACE ( 'NONE', ( #5508 ), #20282, .F. ) ;
#19874=ADVANCED_FACE ( 'NONE', ( #7420 ), #17323, .T. ) ;
#19884=EDGE_CURVE ( 'NONE', #9071, #4581, #5828, .T. ) ;
#19936=LINE ( 'NONE', #3360, #19032 ) ;
#19937=( GEOMETRIC_REPRESENTATION_CONTEXT ( 3 ) GLOBAL_UNCERTAINTY_ASSIGNED_CONTEXT ( ( #7021 ) ) GLOBAL_UNIT_ASSIGNED_CONTEXT ( ( #16252, #9565, #19635 ) ) REPRESENTATION_CONTEXT ( 'NONE', 'WORKASPACE' ) );
#19957=VECTOR ( 'NONE', #16038, 1000.000000000000000 ) ;
#19990=LINE ( 'NONE', #9951, #11330 ) ;
#20053=ADVANCED_FACE ( 'NONE', ( #4542 ), #12533, .T. ) ;
#20070=LINE ( 'NONE', #16998, #18322 ) ;
#20077=CARTESIAN_POINT ( 'NONE',  ( 23.03948732994508575, 43.16218137147969003, 76.90433879953101837 ) ) ;
#20082=VECTOR ( 'NONE', #12033, 1000.000000000000000 ) ;
#20158=EDGE_CURVE ( 'NONE', #13483, #20468, #9768, .T. ) ;
#20196=CARTESIAN_POINT ( 'NONE',  ( 23.03948732994508575, 43.16218137147968292, 78.30433879953099563 ) ) ;
#20247=DIRECTION ( 'NONE',  ( 1.402518428993831676E-16, -1.000000000000000000, 0.000000000000000000 ) ) ;
#20258=EDGE_CURVE ( 'NONE', #15837, #18617, #7113, .T. ) ;
#20265=EDGE_CURVE ( 'NONE', #10795, #4554, #7813, .T. ) ;
#20275=ORIENTED_EDGE ( 'NONE', *, *, #3277, .T. ) ;
#20282=PLANE ( 'NONE',  #5869 ) ;
#20300=VECTOR ( 'NONE', #19476, 1000.000000000000000 ) ;
#20328=VECTOR ( 'NONE', #5775, 1000.000000000000000 ) ;
#20347=EDGE_LOOP ( 'NONE', ( #10166, #6589, #16753, #14950 ) ) ;
#20351=DIRECTION ( 'NONE',  ( -1.402518428993831183E-16, 1.000000000000000000, -3.469446951953617640E-16 ) ) ;
#20360=DIRECTION ( 'NONE',  ( 3.154042683594179047E-15, 0.000000000000000000, -1.000000000000000000 ) ) ;
#20382=DIRECTION ( 'NONE',  ( -1.402518428993831676E-16, 1.000000000000000000, -0.000000000000000000 ) ) ;
#20387=VECTOR ( 'NONE', #5691, 1000.000000000000000 ) ;
#20397=DIRECTION ( 'NONE',  ( -1.402518428993831183E-16, 1.000000000000000000, -3.469446951953617640E-16 ) ) ;
#20410=DIRECTION ( 'NONE',  ( -1.402518428993831183E-16, 1.000000000000000000, -3.469446951953617640E-16 ) ) ;
#20414=EDGE_CURVE ( 'NONE', #14294, #7818, #15497, .T. ) ;
#20423=ADVANCED_FACE ( 'NONE', ( #12507 ), #12715, .F. ) ;
#20441=CIRCLE ( 'NONE', #17399, 1.399999999999995026 ) ;
#20448=ADVANCED_FACE ( 'NONE', ( #17398 ), #6109, .T. ) ;
#20468=VERTEX_POINT ( 'NONE', #18991 ) ;
#20471=ORIENTED_EDGE ( 'NONE', *, *, #18621, .T. ) ;
#20472=CIRCLE ( 'NONE', #6205, 1.399999999999995026 ) ;
#20533=EDGE_CURVE ( 'NONE', #8020, #9071, #19692, .T. ) ;
#20549=DIRECTION ( 'NONE',  ( 0.7071067811865443531, 0.7071067811865506814, -2.453269466693410947E-16 ) ) ;
#20566=EDGE_CURVE ( 'NONE', #9174, #5774, #10216, .T. ) ;
#20576=ORIENTED_EDGE ( 'NONE', *, *, #17449, .T. ) ;
#20591=DIRECTION ( 'NONE',  ( 1.000000000000000000, 0.000000000000000000, 0.000000000000000000 ) ) ;
#20607=CARTESIAN_POINT ( 'NONE',  ( 25.63948732994508362, 45.16218137147969003, 76.90433879953101837 ) ) ;
#20630=ORIENTED_EDGE ( 'NONE', *, *, #7826, .F. ) ;
#20668=EDGE_CURVE ( 'NONE', #12829, #4876, #13320, .T. ) ;
#20704=EDGE_CURVE ( 'NONE', #13369, #9174, #3622, .T. ) ;
#20715=DIRECTION ( 'NONE',  ( -1.402518428993831183E-16, 1.000000000000000000, -3.469446951953617147E-16 ) ) ;
#20738=ORIENTED_EDGE ( 'NONE', *, *, #20533, .F. ) ;
#20749=VERTEX_POINT ( 'NONE', #13625 ) ;
#20774=EDGE_LOOP ( 'NONE', ( #19074, #3184, #20630, #14260, #4625 ) ) ;
#20803=CARTESIAN_POINT ( 'NONE',  ( 26.43948732994507367, 43.16218137147969003, 74.70433879953098710 ) ) ;
#20805=DIRECTION ( 'NONE',  ( 0.7071067811865506814, -0.7071067811865443531, 0.000000000000000000 ) ) ;
#20808=CARTESIAN_POINT ( 'NONE',  ( 24.43948732994508077, 43.16218137147968292, 76.90433879953101837 ) ) ;
#20816=CIRCLE ( 'NONE', #7912, 1.399999999999995026 ) ;
#20835=CARTESIAN_POINT ( 'NONE',  ( 27.03948732994508219, 43.16218137147969003, 75.00433879953099847 ) ) ;
#20861=DIRECTION ( 'NONE',  ( 3.154042683594179442E-15, 0.000000000000000000, -1.000000000000000000 ) ) ;
#20908=PRESENTATION_STYLE_ASSIGNMENT (( #3058 ) ) ;
#20941=FACE_OUTER_BOUND ( 'NONE', #17011, .T. ) ;
#20959=PLANE ( 'NONE',  #4470 ) ;
#20964=FACE_OUTER_BOUND ( 'NONE', #12205, .T. ) ;
#20974=EDGE_LOOP ( 'NONE', ( #14984, #6257, #19852, #8707 ) ) ;
#20976=CARTESIAN_POINT ( 'NONE',  ( 23.63948732994508717, 43.16218137147969003, 74.70433879953098710 ) ) ;
#20996=ORIENTED_EDGE ( 'NONE', *, *, #6765, .T. ) ;
#21012=UNCERTAINTY_MEASURE_WITH_UNIT (LENGTH_MEASURE( 1.000000000000000082E-05 ), #1255, 'distance_accuracy_value', 'NONE');
#21020=ORIENTED_EDGE ( 'NONE', *, *, #14455, .F. ) ;
#21027=ORIENTED_EDGE ( 'NONE', *, *, #12500, .F. ) ;
ENDSEC;
END-ISO-10303-21;
